ISO-10303-21;
HEADER;
/* Generated by software containing ST-Developer
 * from STEP Tools, Inc. (www.steptools.com) 
 */

FILE_DESCRIPTION(
/* description */ (''),
/* implementation_level */ '2;1');

FILE_NAME(
/* name */ 'Motor_Mount (1).step',
/* time_stamp */ '2026-10-22T15:07:41+06:00',
/* author */ (''),
/* organization */ (''),
/* preprocessor_version */ 'ST-DEVELOPER v20.2',
/* originating_system */ 'Autodesk Translation Framework v15.15.0.0',
/* authorisation */ '');

FILE_SCHEMA (('AUTOMOTIVE_DESIGN { 1 0 10303 214 3 1 1 }'));
ENDSEC;

DATA;
#10=MECHANICAL_DESIGN_GEOMETRIC_PRESENTATION_REPRESENTATION('',(#2880),#19220);
#69=SHAPE_REPRESENTATION_RELATIONSHIP('SRR','None',#19272,#83);
#83=ADVANCED_BREP_SHAPE_REPRESENTATION('',(#97),#19208);
#97=MANIFOLD_SOLID_BREP('Motor_Mount',#11316);
#118=FACE_BOUND('',#3478,.T.);
#119=FACE_BOUND('',#3479,.T.);
#120=FACE_BOUND('',#3480,.T.);
#121=FACE_BOUND('',#3481,.T.);
#122=FACE_BOUND('',#3482,.T.);
#123=FACE_BOUND('',#3483,.T.);
#124=FACE_BOUND('',#3484,.T.);
#125=FACE_BOUND('',#3485,.T.);
#126=FACE_BOUND('',#3486,.T.);
#127=FACE_BOUND('',#3487,.T.);
#128=FACE_BOUND('',#3488,.T.);
#129=FACE_BOUND('',#3526,.T.);
#130=FACE_BOUND('',#3527,.T.);
#131=FACE_BOUND('',#3528,.T.);
#132=FACE_BOUND('',#3529,.T.);
#133=FACE_BOUND('',#3530,.T.);
#134=FACE_BOUND('',#3531,.T.);
#135=FACE_BOUND('',#3532,.T.);
#136=FACE_BOUND('',#3533,.T.);
#137=FACE_BOUND('',#3534,.T.);
#138=FACE_BOUND('',#3535,.T.);
#139=FACE_BOUND('',#3536,.T.);
#140=FACE_BOUND('',#3538,.T.);
#141=FACE_BOUND('',#3539,.T.);
#142=FACE_BOUND('',#3540,.T.);
#143=FACE_BOUND('',#3541,.T.);
#144=FACE_BOUND('',#3542,.T.);
#145=FACE_BOUND('',#3543,.T.);
#146=FACE_BOUND('',#3544,.T.);
#147=FACE_BOUND('',#3545,.T.);
#148=FACE_BOUND('',#3546,.T.);
#149=FACE_BOUND('',#3547,.T.);
#150=FACE_BOUND('',#3548,.T.);
#151=FACE_BOUND('',#3551,.T.);
#152=FACE_BOUND('',#3552,.T.);
#153=FACE_BOUND('',#3553,.T.);
#154=FACE_BOUND('',#3554,.T.);
#155=FACE_BOUND('',#3555,.T.);
#156=FACE_BOUND('',#3556,.T.);
#157=FACE_BOUND('',#3557,.T.);
#158=FACE_BOUND('',#3558,.T.);
#159=FACE_BOUND('',#3559,.T.);
#160=FACE_BOUND('',#3560,.T.);
#161=FACE_BOUND('',#3561,.T.);
#162=FACE_BOUND('',#3563,.T.);
#163=FACE_BOUND('',#3564,.T.);
#164=FACE_BOUND('',#3565,.T.);
#165=FACE_BOUND('',#3566,.T.);
#166=FACE_BOUND('',#3567,.T.);
#167=FACE_BOUND('',#3568,.T.);
#168=FACE_BOUND('',#3569,.T.);
#169=FACE_BOUND('',#3570,.T.);
#170=FACE_BOUND('',#3571,.T.);
#171=FACE_BOUND('',#3572,.T.);
#172=FACE_BOUND('',#3573,.T.);
#173=FACE_BOUND('',#3575,.T.);
#174=FACE_BOUND('',#3576,.T.);
#175=FACE_BOUND('',#3577,.T.);
#176=FACE_BOUND('',#3578,.T.);
#177=FACE_BOUND('',#3579,.T.);
#178=FACE_BOUND('',#3580,.T.);
#179=FACE_BOUND('',#3581,.T.);
#180=FACE_BOUND('',#3582,.T.);
#181=FACE_BOUND('',#3583,.T.);
#182=FACE_BOUND('',#3584,.T.);
#183=FACE_BOUND('',#3585,.T.);
#637=PLANE('',#11559);
#638=PLANE('',#11571);
#639=PLANE('',#11663);
#640=PLANE('',#11664);
#641=PLANE('',#11665);
#642=PLANE('',#11666);
#643=PLANE('',#11667);
#644=PLANE('',#11668);
#645=PLANE('',#11669);
#646=PLANE('',#11670);
#851=LINE('',#16197,#1706);
#852=LINE('',#16200,#1707);
#853=LINE('',#16203,#1708);
#854=LINE('',#16205,#1709);
#855=LINE('',#16206,#1710);
#856=LINE('',#16231,#1711);
#857=LINE('',#16233,#1712);
#858=LINE('',#16235,#1713);
#859=LINE('',#16237,#1714);
#860=LINE('',#16239,#1715);
#861=LINE('',#16241,#1716);
#862=LINE('',#16243,#1717);
#863=LINE('',#16248,#1718);
#864=LINE('',#16253,#1719);
#865=LINE('',#16259,#1720);
#866=LINE('',#16265,#1721);
#867=LINE('',#16271,#1722);
#868=LINE('',#16277,#1723);
#869=LINE('',#16283,#1724);
#870=LINE('',#16289,#1725);
#871=LINE('',#16295,#1726);
#872=LINE('',#16301,#1727);
#873=LINE('',#16307,#1728);
#874=LINE('',#16313,#1729);
#875=LINE('',#16317,#1730);
#876=LINE('',#16321,#1731);
#877=LINE('',#16325,#1732);
#878=LINE('',#16329,#1733);
#879=LINE('',#16333,#1734);
#880=LINE('',#16337,#1735);
#881=LINE('',#16341,#1736);
#882=LINE('',#16345,#1737);
#883=LINE('',#16349,#1738);
#884=LINE('',#16353,#1739);
#885=LINE('',#16357,#1740);
#886=LINE('',#16363,#1741);
#887=LINE('',#16369,#1742);
#888=LINE('',#16375,#1743);
#889=LINE('',#16381,#1744);
#890=LINE('',#16387,#1745);
#891=LINE('',#16393,#1746);
#892=LINE('',#16399,#1747);
#893=LINE('',#16405,#1748);
#894=LINE('',#16411,#1749);
#895=LINE('',#16417,#1750);
#896=LINE('',#16423,#1751);
#897=LINE('',#16427,#1752);
#898=LINE('',#16429,#1753);
#899=LINE('',#16430,#1754);
#900=LINE('',#16432,#1755);
#901=LINE('',#16435,#1756);
#902=LINE('',#16436,#1757);
#903=LINE('',#16439,#1758);
#904=LINE('',#16440,#1759);
#905=LINE('',#16443,#1760);
#906=LINE('',#16444,#1761);
#907=LINE('',#16447,#1762);
#908=LINE('',#16448,#1763);
#909=LINE('',#16450,#1764);
#1706=VECTOR('',#12890,10.);
#1707=VECTOR('',#12893,10.);
#1708=VECTOR('',#12896,10.);
#1709=VECTOR('',#12897,10.);
#1710=VECTOR('',#12898,10.);
#1711=VECTOR('',#12923,10.);
#1712=VECTOR('',#12924,10.);
#1713=VECTOR('',#12925,10.);
#1714=VECTOR('',#12926,10.);
#1715=VECTOR('',#12927,10.);
#1716=VECTOR('',#12928,10.);
#1717=VECTOR('',#12929,10.);
#1718=VECTOR('',#12936,10.);
#1719=VECTOR('',#12941,2.5);
#1720=VECTOR('',#12948,2.5);
#1721=VECTOR('',#12955,2.5);
#1722=VECTOR('',#12962,7.5);
#1723=VECTOR('',#12969,2.5);
#1724=VECTOR('',#12976,2.5);
#1725=VECTOR('',#12983,2.5);
#1726=VECTOR('',#12990,2.5);
#1727=VECTOR('',#12997,2.5);
#1728=VECTOR('',#13004,2.5);
#1729=VECTOR('',#13011,2.5);
#1730=VECTOR('',#13016,2.5);
#1731=VECTOR('',#13021,2.5);
#1732=VECTOR('',#13026,2.5);
#1733=VECTOR('',#13031,2.5);
#1734=VECTOR('',#13036,2.5);
#1735=VECTOR('',#13041,2.5);
#1736=VECTOR('',#13046,2.5);
#1737=VECTOR('',#13051,7.5);
#1738=VECTOR('',#13056,2.5);
#1739=VECTOR('',#13061,2.5);
#1740=VECTOR('',#13066,2.5);
#1741=VECTOR('',#13073,2.5);
#1742=VECTOR('',#13080,2.5);
#1743=VECTOR('',#13087,2.5);
#1744=VECTOR('',#13094,7.5);
#1745=VECTOR('',#13101,2.5);
#1746=VECTOR('',#13108,2.5);
#1747=VECTOR('',#13115,2.5);
#1748=VECTOR('',#13122,2.5);
#1749=VECTOR('',#13129,2.5);
#1750=VECTOR('',#13136,2.5);
#1751=VECTOR('',#13143,2.5);
#1752=VECTOR('',#13148,10.);
#1753=VECTOR('',#13149,10.);
#1754=VECTOR('',#13150,10.);
#1755=VECTOR('',#13153,10.);
#1756=VECTOR('',#13156,10.);
#1757=VECTOR('',#13157,10.);
#1758=VECTOR('',#13160,10.);
#1759=VECTOR('',#13161,10.);
#1760=VECTOR('',#13164,10.);
#1761=VECTOR('',#13165,10.);
#1762=VECTOR('',#13168,10.);
#1763=VECTOR('',#13169,10.);
#1764=VECTOR('',#13172,10.);
#2561=CYLINDRICAL_SURFACE('',#11556,1.);
#2562=CYLINDRICAL_SURFACE('',#11573,1.);
#2563=CYLINDRICAL_SURFACE('',#11575,2.5);
#2564=CYLINDRICAL_SURFACE('',#11578,2.5);
#2565=CYLINDRICAL_SURFACE('',#11581,2.5);
#2566=CYLINDRICAL_SURFACE('',#11584,7.5);
#2567=CYLINDRICAL_SURFACE('',#11587,2.5);
#2568=CYLINDRICAL_SURFACE('',#11590,2.5);
#2569=CYLINDRICAL_SURFACE('',#11593,2.5);
#2570=CYLINDRICAL_SURFACE('',#11596,2.5);
#2571=CYLINDRICAL_SURFACE('',#11599,2.5);
#2572=CYLINDRICAL_SURFACE('',#11602,2.5);
#2573=CYLINDRICAL_SURFACE('',#11605,2.5);
#2574=CYLINDRICAL_SURFACE('',#11608,2.5);
#2575=CYLINDRICAL_SURFACE('',#11610,2.5);
#2576=CYLINDRICAL_SURFACE('',#11612,2.5);
#2577=CYLINDRICAL_SURFACE('',#11614,2.5);
#2578=CYLINDRICAL_SURFACE('',#11616,2.5);
#2579=CYLINDRICAL_SURFACE('',#11618,2.5);
#2580=CYLINDRICAL_SURFACE('',#11620,2.5);
#2581=CYLINDRICAL_SURFACE('',#11622,7.5);
#2582=CYLINDRICAL_SURFACE('',#11624,2.5);
#2583=CYLINDRICAL_SURFACE('',#11626,2.5);
#2584=CYLINDRICAL_SURFACE('',#11628,2.5);
#2585=CYLINDRICAL_SURFACE('',#11630,2.5);
#2586=CYLINDRICAL_SURFACE('',#11633,2.5);
#2587=CYLINDRICAL_SURFACE('',#11636,2.5);
#2588=CYLINDRICAL_SURFACE('',#11639,7.5);
#2589=CYLINDRICAL_SURFACE('',#11642,2.5);
#2590=CYLINDRICAL_SURFACE('',#11645,2.5);
#2591=CYLINDRICAL_SURFACE('',#11648,2.5);
#2592=CYLINDRICAL_SURFACE('',#11651,2.5);
#2593=CYLINDRICAL_SURFACE('',#11654,2.5);
#2594=CYLINDRICAL_SURFACE('',#11657,2.5);
#2595=CYLINDRICAL_SURFACE('',#11660,2.5);
#2880=STYLED_ITEM('',(#19417),#97);
#2921=FACE_OUTER_BOUND('',#3476,.T.);
#2922=FACE_OUTER_BOUND('',#3477,.T.);
#2923=FACE_OUTER_BOUND('',#3489,.T.);
#2924=FACE_OUTER_BOUND('',#3490,.T.);
#2925=FACE_OUTER_BOUND('',#3491,.T.);
#2926=FACE_OUTER_BOUND('',#3492,.T.);
#2927=FACE_OUTER_BOUND('',#3493,.T.);
#2928=FACE_OUTER_BOUND('',#3494,.T.);
#2929=FACE_OUTER_BOUND('',#3495,.T.);
#2930=FACE_OUTER_BOUND('',#3496,.T.);
#2931=FACE_OUTER_BOUND('',#3497,.T.);
#2932=FACE_OUTER_BOUND('',#3498,.T.);
#2933=FACE_OUTER_BOUND('',#3499,.T.);
#2934=FACE_OUTER_BOUND('',#3500,.T.);
#2935=FACE_OUTER_BOUND('',#3501,.T.);
#2936=FACE_OUTER_BOUND('',#3502,.T.);
#2937=FACE_OUTER_BOUND('',#3503,.T.);
#2938=FACE_OUTER_BOUND('',#3504,.T.);
#2939=FACE_OUTER_BOUND('',#3505,.T.);
#2940=FACE_OUTER_BOUND('',#3506,.T.);
#2941=FACE_OUTER_BOUND('',#3507,.T.);
#2942=FACE_OUTER_BOUND('',#3508,.T.);
#2943=FACE_OUTER_BOUND('',#3509,.T.);
#2944=FACE_OUTER_BOUND('',#3510,.T.);
#2945=FACE_OUTER_BOUND('',#3511,.T.);
#2946=FACE_OUTER_BOUND('',#3512,.T.);
#2947=FACE_OUTER_BOUND('',#3513,.T.);
#2948=FACE_OUTER_BOUND('',#3514,.T.);
#2949=FACE_OUTER_BOUND('',#3515,.T.);
#2950=FACE_OUTER_BOUND('',#3516,.T.);
#2951=FACE_OUTER_BOUND('',#3517,.T.);
#2952=FACE_OUTER_BOUND('',#3518,.T.);
#2953=FACE_OUTER_BOUND('',#3519,.T.);
#2954=FACE_OUTER_BOUND('',#3520,.T.);
#2955=FACE_OUTER_BOUND('',#3521,.T.);
#2956=FACE_OUTER_BOUND('',#3522,.T.);
#2957=FACE_OUTER_BOUND('',#3523,.T.);
#2958=FACE_OUTER_BOUND('',#3524,.T.);
#2959=FACE_OUTER_BOUND('',#3525,.T.);
#2960=FACE_OUTER_BOUND('',#3537,.T.);
#2961=FACE_OUTER_BOUND('',#3549,.T.);
#2962=FACE_OUTER_BOUND('',#3550,.T.);
#2963=FACE_OUTER_BOUND('',#3562,.T.);
#2964=FACE_OUTER_BOUND('',#3574,.T.);
#2965=FACE_OUTER_BOUND('',#3586,.T.);
#3476=EDGE_LOOP('',(#7816,#7817,#7818,#7819));
#3477=EDGE_LOOP('',(#7820,#7821,#7822,#7823));
#3478=EDGE_LOOP('',(#7824));
#3479=EDGE_LOOP('',(#7825));
#3480=EDGE_LOOP('',(#7826));
#3481=EDGE_LOOP('',(#7827));
#3482=EDGE_LOOP('',(#7828));
#3483=EDGE_LOOP('',(#7829));
#3484=EDGE_LOOP('',(#7830));
#3485=EDGE_LOOP('',(#7831));
#3486=EDGE_LOOP('',(#7832));
#3487=EDGE_LOOP('',(#7833));
#3488=EDGE_LOOP('',(#7834));
#3489=EDGE_LOOP('',(#7835,#7836,#7837,#7838,#7839,#7840,#7841,#7842,#7843,
#7844));
#3490=EDGE_LOOP('',(#7845,#7846,#7847,#7848));
#3491=EDGE_LOOP('',(#7849,#7850,#7851,#7852));
#3492=EDGE_LOOP('',(#7853,#7854,#7855,#7856));
#3493=EDGE_LOOP('',(#7857,#7858,#7859,#7860));
#3494=EDGE_LOOP('',(#7861,#7862,#7863,#7864));
#3495=EDGE_LOOP('',(#7865,#7866,#7867,#7868));
#3496=EDGE_LOOP('',(#7869,#7870,#7871,#7872));
#3497=EDGE_LOOP('',(#7873,#7874,#7875,#7876));
#3498=EDGE_LOOP('',(#7877,#7878,#7879,#7880));
#3499=EDGE_LOOP('',(#7881,#7882,#7883,#7884));
#3500=EDGE_LOOP('',(#7885,#7886,#7887,#7888));
#3501=EDGE_LOOP('',(#7889,#7890,#7891,#7892));
#3502=EDGE_LOOP('',(#7893,#7894,#7895,#7896));
#3503=EDGE_LOOP('',(#7897,#7898,#7899,#7900));
#3504=EDGE_LOOP('',(#7901,#7902,#7903,#7904));
#3505=EDGE_LOOP('',(#7905,#7906,#7907,#7908));
#3506=EDGE_LOOP('',(#7909,#7910,#7911,#7912));
#3507=EDGE_LOOP('',(#7913,#7914,#7915,#7916));
#3508=EDGE_LOOP('',(#7917,#7918,#7919,#7920));
#3509=EDGE_LOOP('',(#7921,#7922,#7923,#7924));
#3510=EDGE_LOOP('',(#7925,#7926,#7927,#7928));
#3511=EDGE_LOOP('',(#7929,#7930,#7931,#7932));
#3512=EDGE_LOOP('',(#7933,#7934,#7935,#7936));
#3513=EDGE_LOOP('',(#7937,#7938,#7939,#7940));
#3514=EDGE_LOOP('',(#7941,#7942,#7943,#7944));
#3515=EDGE_LOOP('',(#7945,#7946,#7947,#7948));
#3516=EDGE_LOOP('',(#7949,#7950,#7951,#7952));
#3517=EDGE_LOOP('',(#7953,#7954,#7955,#7956));
#3518=EDGE_LOOP('',(#7957,#7958,#7959,#7960));
#3519=EDGE_LOOP('',(#7961,#7962,#7963,#7964));
#3520=EDGE_LOOP('',(#7965,#7966,#7967,#7968));
#3521=EDGE_LOOP('',(#7969,#7970,#7971,#7972));
#3522=EDGE_LOOP('',(#7973,#7974,#7975,#7976));
#3523=EDGE_LOOP('',(#7977,#7978,#7979,#7980));
#3524=EDGE_LOOP('',(#7981,#7982,#7983,#7984));
#3525=EDGE_LOOP('',(#7985,#7986,#7987,#7988));
#3526=EDGE_LOOP('',(#7989));
#3527=EDGE_LOOP('',(#7990));
#3528=EDGE_LOOP('',(#7991));
#3529=EDGE_LOOP('',(#7992));
#3530=EDGE_LOOP('',(#7993));
#3531=EDGE_LOOP('',(#7994));
#3532=EDGE_LOOP('',(#7995));
#3533=EDGE_LOOP('',(#7996));
#3534=EDGE_LOOP('',(#7997));
#3535=EDGE_LOOP('',(#7998));
#3536=EDGE_LOOP('',(#7999));
#3537=EDGE_LOOP('',(#8000,#8001,#8002,#8003));
#3538=EDGE_LOOP('',(#8004));
#3539=EDGE_LOOP('',(#8005));
#3540=EDGE_LOOP('',(#8006));
#3541=EDGE_LOOP('',(#8007));
#3542=EDGE_LOOP('',(#8008));
#3543=EDGE_LOOP('',(#8009));
#3544=EDGE_LOOP('',(#8010));
#3545=EDGE_LOOP('',(#8011));
#3546=EDGE_LOOP('',(#8012));
#3547=EDGE_LOOP('',(#8013));
#3548=EDGE_LOOP('',(#8014));
#3549=EDGE_LOOP('',(#8015,#8016,#8017,#8018));
#3550=EDGE_LOOP('',(#8019,#8020,#8021,#8022));
#3551=EDGE_LOOP('',(#8023));
#3552=EDGE_LOOP('',(#8024));
#3553=EDGE_LOOP('',(#8025));
#3554=EDGE_LOOP('',(#8026));
#3555=EDGE_LOOP('',(#8027));
#3556=EDGE_LOOP('',(#8028));
#3557=EDGE_LOOP('',(#8029));
#3558=EDGE_LOOP('',(#8030));
#3559=EDGE_LOOP('',(#8031));
#3560=EDGE_LOOP('',(#8032));
#3561=EDGE_LOOP('',(#8033));
#3562=EDGE_LOOP('',(#8034,#8035,#8036,#8037));
#3563=EDGE_LOOP('',(#8038));
#3564=EDGE_LOOP('',(#8039));
#3565=EDGE_LOOP('',(#8040));
#3566=EDGE_LOOP('',(#8041));
#3567=EDGE_LOOP('',(#8042));
#3568=EDGE_LOOP('',(#8043));
#3569=EDGE_LOOP('',(#8044));
#3570=EDGE_LOOP('',(#8045));
#3571=EDGE_LOOP('',(#8046));
#3572=EDGE_LOOP('',(#8047));
#3573=EDGE_LOOP('',(#8048));
#3574=EDGE_LOOP('',(#8049,#8050,#8051,#8052));
#3575=EDGE_LOOP('',(#8053));
#3576=EDGE_LOOP('',(#8054));
#3577=EDGE_LOOP('',(#8055));
#3578=EDGE_LOOP('',(#8056));
#3579=EDGE_LOOP('',(#8057));
#3580=EDGE_LOOP('',(#8058));
#3581=EDGE_LOOP('',(#8059));
#3582=EDGE_LOOP('',(#8060));
#3583=EDGE_LOOP('',(#8061));
#3584=EDGE_LOOP('',(#8062));
#3585=EDGE_LOOP('',(#8063));
#3586=EDGE_LOOP('',(#8064,#8065,#8066,#8067,#8068,#8069,#8070,#8071,#8072,
#8073));
#4541=CIRCLE('',#11557,1.);
#4542=CIRCLE('',#11558,1.);
#4543=CIRCLE('',#11560,2.5);
#4544=CIRCLE('',#11561,2.5);
#4545=CIRCLE('',#11562,2.5);
#4546=CIRCLE('',#11563,7.5);
#4547=CIRCLE('',#11564,2.5);
#4548=CIRCLE('',#11565,2.5);
#4549=CIRCLE('',#11566,2.5);
#4550=CIRCLE('',#11567,2.5);
#4551=CIRCLE('',#11568,2.5);
#4552=CIRCLE('',#11569,2.5);
#4553=CIRCLE('',#11570,2.5);
#4554=CIRCLE('',#11572,1.);
#4555=CIRCLE('',#11574,1.);
#4556=CIRCLE('',#11576,2.5);
#4557=CIRCLE('',#11577,2.5);
#4558=CIRCLE('',#11579,2.5);
#4559=CIRCLE('',#11580,2.5);
#4560=CIRCLE('',#11582,2.5);
#4561=CIRCLE('',#11583,2.5);
#4562=CIRCLE('',#11585,7.5);
#4563=CIRCLE('',#11586,7.5);
#4564=CIRCLE('',#11588,2.5);
#4565=CIRCLE('',#11589,2.5);
#4566=CIRCLE('',#11591,2.5);
#4567=CIRCLE('',#11592,2.5);
#4568=CIRCLE('',#11594,2.5);
#4569=CIRCLE('',#11595,2.5);
#4570=CIRCLE('',#11597,2.5);
#4571=CIRCLE('',#11598,2.5);
#4572=CIRCLE('',#11600,2.5);
#4573=CIRCLE('',#11601,2.5);
#4574=CIRCLE('',#11603,2.5);
#4575=CIRCLE('',#11604,2.5);
#4576=CIRCLE('',#11606,2.5);
#4577=CIRCLE('',#11607,2.5);
#4578=CIRCLE('',#11609,2.5);
#4579=CIRCLE('',#11611,2.5);
#4580=CIRCLE('',#11613,2.5);
#4581=CIRCLE('',#11615,2.5);
#4582=CIRCLE('',#11617,2.5);
#4583=CIRCLE('',#11619,2.5);
#4584=CIRCLE('',#11621,2.5);
#4585=CIRCLE('',#11623,7.5);
#4586=CIRCLE('',#11625,2.5);
#4587=CIRCLE('',#11627,2.5);
#4588=CIRCLE('',#11629,2.5);
#4589=CIRCLE('',#11631,2.5);
#4590=CIRCLE('',#11632,2.5);
#4591=CIRCLE('',#11634,2.5);
#4592=CIRCLE('',#11635,2.5);
#4593=CIRCLE('',#11637,2.5);
#4594=CIRCLE('',#11638,2.5);
#4595=CIRCLE('',#11640,7.5);
#4596=CIRCLE('',#11641,7.5);
#4597=CIRCLE('',#11643,2.5);
#4598=CIRCLE('',#11644,2.5);
#4599=CIRCLE('',#11646,2.5);
#4600=CIRCLE('',#11647,2.5);
#4601=CIRCLE('',#11649,2.5);
#4602=CIRCLE('',#11650,2.5);
#4603=CIRCLE('',#11652,2.5);
#4604=CIRCLE('',#11653,2.5);
#4605=CIRCLE('',#11655,2.5);
#4606=CIRCLE('',#11656,2.5);
#4607=CIRCLE('',#11658,2.5);
#4608=CIRCLE('',#11659,2.5);
#4609=CIRCLE('',#11661,2.5);
#4610=CIRCLE('',#11662,2.5);
#5205=VERTEX_POINT('',#16193);
#5206=VERTEX_POINT('',#16194);
#5207=VERTEX_POINT('',#16196);
#5208=VERTEX_POINT('',#16198);
#5209=VERTEX_POINT('',#16202);
#5210=VERTEX_POINT('',#16204);
#5211=VERTEX_POINT('',#16207);
#5212=VERTEX_POINT('',#16209);
#5213=VERTEX_POINT('',#16211);
#5214=VERTEX_POINT('',#16213);
#5215=VERTEX_POINT('',#16215);
#5216=VERTEX_POINT('',#16217);
#5217=VERTEX_POINT('',#16219);
#5218=VERTEX_POINT('',#16221);
#5219=VERTEX_POINT('',#16223);
#5220=VERTEX_POINT('',#16225);
#5221=VERTEX_POINT('',#16227);
#5222=VERTEX_POINT('',#16230);
#5223=VERTEX_POINT('',#16232);
#5224=VERTEX_POINT('',#16234);
#5225=VERTEX_POINT('',#16236);
#5226=VERTEX_POINT('',#16238);
#5227=VERTEX_POINT('',#16240);
#5228=VERTEX_POINT('',#16242);
#5229=VERTEX_POINT('',#16246);
#5230=VERTEX_POINT('',#16250);
#5231=VERTEX_POINT('',#16252);
#5232=VERTEX_POINT('',#16256);
#5233=VERTEX_POINT('',#16258);
#5234=VERTEX_POINT('',#16262);
#5235=VERTEX_POINT('',#16264);
#5236=VERTEX_POINT('',#16268);
#5237=VERTEX_POINT('',#16270);
#5238=VERTEX_POINT('',#16274);
#5239=VERTEX_POINT('',#16276);
#5240=VERTEX_POINT('',#16280);
#5241=VERTEX_POINT('',#16282);
#5242=VERTEX_POINT('',#16286);
#5243=VERTEX_POINT('',#16288);
#5244=VERTEX_POINT('',#16292);
#5245=VERTEX_POINT('',#16294);
#5246=VERTEX_POINT('',#16298);
#5247=VERTEX_POINT('',#16300);
#5248=VERTEX_POINT('',#16304);
#5249=VERTEX_POINT('',#16306);
#5250=VERTEX_POINT('',#16310);
#5251=VERTEX_POINT('',#16312);
#5252=VERTEX_POINT('',#16316);
#5253=VERTEX_POINT('',#16320);
#5254=VERTEX_POINT('',#16324);
#5255=VERTEX_POINT('',#16328);
#5256=VERTEX_POINT('',#16332);
#5257=VERTEX_POINT('',#16336);
#5258=VERTEX_POINT('',#16340);
#5259=VERTEX_POINT('',#16344);
#5260=VERTEX_POINT('',#16348);
#5261=VERTEX_POINT('',#16352);
#5262=VERTEX_POINT('',#16356);
#5263=VERTEX_POINT('',#16360);
#5264=VERTEX_POINT('',#16362);
#5265=VERTEX_POINT('',#16366);
#5266=VERTEX_POINT('',#16368);
#5267=VERTEX_POINT('',#16372);
#5268=VERTEX_POINT('',#16374);
#5269=VERTEX_POINT('',#16378);
#5270=VERTEX_POINT('',#16380);
#5271=VERTEX_POINT('',#16384);
#5272=VERTEX_POINT('',#16386);
#5273=VERTEX_POINT('',#16390);
#5274=VERTEX_POINT('',#16392);
#5275=VERTEX_POINT('',#16396);
#5276=VERTEX_POINT('',#16398);
#5277=VERTEX_POINT('',#16402);
#5278=VERTEX_POINT('',#16404);
#5279=VERTEX_POINT('',#16408);
#5280=VERTEX_POINT('',#16410);
#5281=VERTEX_POINT('',#16414);
#5282=VERTEX_POINT('',#16416);
#5283=VERTEX_POINT('',#16420);
#5284=VERTEX_POINT('',#16422);
#5285=VERTEX_POINT('',#16426);
#5286=VERTEX_POINT('',#16428);
#5287=VERTEX_POINT('',#16434);
#5288=VERTEX_POINT('',#16438);
#5289=VERTEX_POINT('',#16442);
#5290=VERTEX_POINT('',#16446);
#6239=EDGE_CURVE('',#5205,#5206,#4541,.T.);
#6240=EDGE_CURVE('',#5206,#5207,#851,.T.);
#6241=EDGE_CURVE('',#5207,#5208,#4542,.T.);
#6242=EDGE_CURVE('',#5208,#5205,#852,.T.);
#6243=EDGE_CURVE('',#5209,#5208,#853,.T.);
#6244=EDGE_CURVE('',#5210,#5209,#854,.T.);
#6245=EDGE_CURVE('',#5205,#5210,#855,.T.);
#6246=EDGE_CURVE('',#5211,#5211,#4543,.T.);
#6247=EDGE_CURVE('',#5212,#5212,#4544,.T.);
#6248=EDGE_CURVE('',#5213,#5213,#4545,.T.);
#6249=EDGE_CURVE('',#5214,#5214,#4546,.T.);
#6250=EDGE_CURVE('',#5215,#5215,#4547,.T.);
#6251=EDGE_CURVE('',#5216,#5216,#4548,.T.);
#6252=EDGE_CURVE('',#5217,#5217,#4549,.T.);
#6253=EDGE_CURVE('',#5218,#5218,#4550,.T.);
#6254=EDGE_CURVE('',#5219,#5219,#4551,.T.);
#6255=EDGE_CURVE('',#5220,#5220,#4552,.T.);
#6256=EDGE_CURVE('',#5221,#5221,#4553,.T.);
#6257=EDGE_CURVE('',#5207,#5222,#856,.T.);
#6258=EDGE_CURVE('',#5222,#5223,#857,.T.);
#6259=EDGE_CURVE('',#5224,#5223,#858,.T.);
#6260=EDGE_CURVE('',#5225,#5224,#859,.T.);
#6261=EDGE_CURVE('',#5226,#5225,#860,.T.);
#6262=EDGE_CURVE('',#5226,#5227,#861,.T.);
#6263=EDGE_CURVE('',#5227,#5228,#862,.T.);
#6264=EDGE_CURVE('',#5209,#5228,#4554,.T.);
#6265=EDGE_CURVE('',#5229,#5210,#4555,.T.);
#6266=EDGE_CURVE('',#5228,#5229,#863,.T.);
#6267=EDGE_CURVE('',#5230,#5230,#4556,.T.);
#6268=EDGE_CURVE('',#5230,#5231,#864,.T.);
#6269=EDGE_CURVE('',#5231,#5231,#4557,.T.);
#6270=EDGE_CURVE('',#5232,#5232,#4558,.T.);
#6271=EDGE_CURVE('',#5232,#5233,#865,.T.);
#6272=EDGE_CURVE('',#5233,#5233,#4559,.T.);
#6273=EDGE_CURVE('',#5234,#5234,#4560,.T.);
#6274=EDGE_CURVE('',#5234,#5235,#866,.T.);
#6275=EDGE_CURVE('',#5235,#5235,#4561,.T.);
#6276=EDGE_CURVE('',#5236,#5236,#4562,.T.);
#6277=EDGE_CURVE('',#5236,#5237,#867,.T.);
#6278=EDGE_CURVE('',#5237,#5237,#4563,.T.);
#6279=EDGE_CURVE('',#5238,#5238,#4564,.T.);
#6280=EDGE_CURVE('',#5238,#5239,#868,.T.);
#6281=EDGE_CURVE('',#5239,#5239,#4565,.T.);
#6282=EDGE_CURVE('',#5240,#5240,#4566,.T.);
#6283=EDGE_CURVE('',#5240,#5241,#869,.T.);
#6284=EDGE_CURVE('',#5241,#5241,#4567,.T.);
#6285=EDGE_CURVE('',#5242,#5242,#4568,.T.);
#6286=EDGE_CURVE('',#5242,#5243,#870,.T.);
#6287=EDGE_CURVE('',#5243,#5243,#4569,.T.);
#6288=EDGE_CURVE('',#5244,#5244,#4570,.T.);
#6289=EDGE_CURVE('',#5244,#5245,#871,.T.);
#6290=EDGE_CURVE('',#5245,#5245,#4571,.T.);
#6291=EDGE_CURVE('',#5246,#5246,#4572,.T.);
#6292=EDGE_CURVE('',#5246,#5247,#872,.T.);
#6293=EDGE_CURVE('',#5247,#5247,#4573,.T.);
#6294=EDGE_CURVE('',#5248,#5248,#4574,.T.);
#6295=EDGE_CURVE('',#5248,#5249,#873,.T.);
#6296=EDGE_CURVE('',#5249,#5249,#4575,.T.);
#6297=EDGE_CURVE('',#5250,#5250,#4576,.T.);
#6298=EDGE_CURVE('',#5250,#5251,#874,.T.);
#6299=EDGE_CURVE('',#5251,#5251,#4577,.T.);
#6300=EDGE_CURVE('',#5221,#5252,#875,.T.);
#6301=EDGE_CURVE('',#5252,#5252,#4578,.T.);
#6302=EDGE_CURVE('',#5220,#5253,#876,.T.);
#6303=EDGE_CURVE('',#5253,#5253,#4579,.T.);
#6304=EDGE_CURVE('',#5219,#5254,#877,.T.);
#6305=EDGE_CURVE('',#5254,#5254,#4580,.T.);
#6306=EDGE_CURVE('',#5218,#5255,#878,.T.);
#6307=EDGE_CURVE('',#5255,#5255,#4581,.T.);
#6308=EDGE_CURVE('',#5217,#5256,#879,.T.);
#6309=EDGE_CURVE('',#5256,#5256,#4582,.T.);
#6310=EDGE_CURVE('',#5216,#5257,#880,.T.);
#6311=EDGE_CURVE('',#5257,#5257,#4583,.T.);
#6312=EDGE_CURVE('',#5215,#5258,#881,.T.);
#6313=EDGE_CURVE('',#5258,#5258,#4584,.T.);
#6314=EDGE_CURVE('',#5214,#5259,#882,.T.);
#6315=EDGE_CURVE('',#5259,#5259,#4585,.T.);
#6316=EDGE_CURVE('',#5213,#5260,#883,.T.);
#6317=EDGE_CURVE('',#5260,#5260,#4586,.T.);
#6318=EDGE_CURVE('',#5212,#5261,#884,.T.);
#6319=EDGE_CURVE('',#5261,#5261,#4587,.T.);
#6320=EDGE_CURVE('',#5211,#5262,#885,.T.);
#6321=EDGE_CURVE('',#5262,#5262,#4588,.T.);
#6322=EDGE_CURVE('',#5263,#5263,#4589,.T.);
#6323=EDGE_CURVE('',#5263,#5264,#886,.T.);
#6324=EDGE_CURVE('',#5264,#5264,#4590,.T.);
#6325=EDGE_CURVE('',#5265,#5265,#4591,.T.);
#6326=EDGE_CURVE('',#5265,#5266,#887,.T.);
#6327=EDGE_CURVE('',#5266,#5266,#4592,.T.);
#6328=EDGE_CURVE('',#5267,#5267,#4593,.T.);
#6329=EDGE_CURVE('',#5267,#5268,#888,.T.);
#6330=EDGE_CURVE('',#5268,#5268,#4594,.T.);
#6331=EDGE_CURVE('',#5269,#5269,#4595,.T.);
#6332=EDGE_CURVE('',#5269,#5270,#889,.T.);
#6333=EDGE_CURVE('',#5270,#5270,#4596,.T.);
#6334=EDGE_CURVE('',#5271,#5271,#4597,.T.);
#6335=EDGE_CURVE('',#5271,#5272,#890,.T.);
#6336=EDGE_CURVE('',#5272,#5272,#4598,.T.);
#6337=EDGE_CURVE('',#5273,#5273,#4599,.T.);
#6338=EDGE_CURVE('',#5273,#5274,#891,.T.);
#6339=EDGE_CURVE('',#5274,#5274,#4600,.T.);
#6340=EDGE_CURVE('',#5275,#5275,#4601,.T.);
#6341=EDGE_CURVE('',#5275,#5276,#892,.T.);
#6342=EDGE_CURVE('',#5276,#5276,#4602,.T.);
#6343=EDGE_CURVE('',#5277,#5277,#4603,.T.);
#6344=EDGE_CURVE('',#5277,#5278,#893,.T.);
#6345=EDGE_CURVE('',#5278,#5278,#4604,.T.);
#6346=EDGE_CURVE('',#5279,#5279,#4605,.T.);
#6347=EDGE_CURVE('',#5279,#5280,#894,.T.);
#6348=EDGE_CURVE('',#5280,#5280,#4606,.T.);
#6349=EDGE_CURVE('',#5281,#5281,#4607,.T.);
#6350=EDGE_CURVE('',#5281,#5282,#895,.T.);
#6351=EDGE_CURVE('',#5282,#5282,#4608,.T.);
#6352=EDGE_CURVE('',#5283,#5283,#4609,.T.);
#6353=EDGE_CURVE('',#5283,#5284,#896,.T.);
#6354=EDGE_CURVE('',#5284,#5284,#4610,.T.);
#6355=EDGE_CURVE('',#5226,#5285,#897,.T.);
#6356=EDGE_CURVE('',#5286,#5285,#898,.T.);
#6357=EDGE_CURVE('',#5227,#5286,#899,.T.);
#6358=EDGE_CURVE('',#5229,#5286,#900,.T.);
#6359=EDGE_CURVE('',#5287,#5206,#901,.T.);
#6360=EDGE_CURVE('',#5222,#5287,#902,.T.);
#6361=EDGE_CURVE('',#5288,#5287,#903,.T.);
#6362=EDGE_CURVE('',#5223,#5288,#904,.T.);
#6363=EDGE_CURVE('',#5289,#5288,#905,.T.);
#6364=EDGE_CURVE('',#5224,#5289,#906,.T.);
#6365=EDGE_CURVE('',#5290,#5289,#907,.T.);
#6366=EDGE_CURVE('',#5225,#5290,#908,.T.);
#6367=EDGE_CURVE('',#5285,#5290,#909,.T.);
#7816=ORIENTED_EDGE('',*,*,#6239,.T.);
#7817=ORIENTED_EDGE('',*,*,#6240,.T.);
#7818=ORIENTED_EDGE('',*,*,#6241,.T.);
#7819=ORIENTED_EDGE('',*,*,#6242,.T.);
#7820=ORIENTED_EDGE('',*,*,#6242,.F.);
#7821=ORIENTED_EDGE('',*,*,#6243,.F.);
#7822=ORIENTED_EDGE('',*,*,#6244,.F.);
#7823=ORIENTED_EDGE('',*,*,#6245,.F.);
#7824=ORIENTED_EDGE('',*,*,#6246,.T.);
#7825=ORIENTED_EDGE('',*,*,#6247,.T.);
#7826=ORIENTED_EDGE('',*,*,#6248,.T.);
#7827=ORIENTED_EDGE('',*,*,#6249,.T.);
#7828=ORIENTED_EDGE('',*,*,#6250,.T.);
#7829=ORIENTED_EDGE('',*,*,#6251,.T.);
#7830=ORIENTED_EDGE('',*,*,#6252,.T.);
#7831=ORIENTED_EDGE('',*,*,#6253,.T.);
#7832=ORIENTED_EDGE('',*,*,#6254,.T.);
#7833=ORIENTED_EDGE('',*,*,#6255,.T.);
#7834=ORIENTED_EDGE('',*,*,#6256,.T.);
#7835=ORIENTED_EDGE('',*,*,#6241,.F.);
#7836=ORIENTED_EDGE('',*,*,#6257,.T.);
#7837=ORIENTED_EDGE('',*,*,#6258,.T.);
#7838=ORIENTED_EDGE('',*,*,#6259,.F.);
#7839=ORIENTED_EDGE('',*,*,#6260,.F.);
#7840=ORIENTED_EDGE('',*,*,#6261,.F.);
#7841=ORIENTED_EDGE('',*,*,#6262,.T.);
#7842=ORIENTED_EDGE('',*,*,#6263,.T.);
#7843=ORIENTED_EDGE('',*,*,#6264,.F.);
#7844=ORIENTED_EDGE('',*,*,#6243,.T.);
#7845=ORIENTED_EDGE('',*,*,#6265,.T.);
#7846=ORIENTED_EDGE('',*,*,#6244,.T.);
#7847=ORIENTED_EDGE('',*,*,#6264,.T.);
#7848=ORIENTED_EDGE('',*,*,#6266,.T.);
#7849=ORIENTED_EDGE('',*,*,#6267,.F.);
#7850=ORIENTED_EDGE('',*,*,#6268,.T.);
#7851=ORIENTED_EDGE('',*,*,#6269,.F.);
#7852=ORIENTED_EDGE('',*,*,#6268,.F.);
#7853=ORIENTED_EDGE('',*,*,#6270,.F.);
#7854=ORIENTED_EDGE('',*,*,#6271,.T.);
#7855=ORIENTED_EDGE('',*,*,#6272,.F.);
#7856=ORIENTED_EDGE('',*,*,#6271,.F.);
#7857=ORIENTED_EDGE('',*,*,#6273,.F.);
#7858=ORIENTED_EDGE('',*,*,#6274,.T.);
#7859=ORIENTED_EDGE('',*,*,#6275,.F.);
#7860=ORIENTED_EDGE('',*,*,#6274,.F.);
#7861=ORIENTED_EDGE('',*,*,#6276,.F.);
#7862=ORIENTED_EDGE('',*,*,#6277,.T.);
#7863=ORIENTED_EDGE('',*,*,#6278,.F.);
#7864=ORIENTED_EDGE('',*,*,#6277,.F.);
#7865=ORIENTED_EDGE('',*,*,#6279,.F.);
#7866=ORIENTED_EDGE('',*,*,#6280,.T.);
#7867=ORIENTED_EDGE('',*,*,#6281,.F.);
#7868=ORIENTED_EDGE('',*,*,#6280,.F.);
#7869=ORIENTED_EDGE('',*,*,#6282,.F.);
#7870=ORIENTED_EDGE('',*,*,#6283,.T.);
#7871=ORIENTED_EDGE('',*,*,#6284,.F.);
#7872=ORIENTED_EDGE('',*,*,#6283,.F.);
#7873=ORIENTED_EDGE('',*,*,#6285,.F.);
#7874=ORIENTED_EDGE('',*,*,#6286,.T.);
#7875=ORIENTED_EDGE('',*,*,#6287,.F.);
#7876=ORIENTED_EDGE('',*,*,#6286,.F.);
#7877=ORIENTED_EDGE('',*,*,#6288,.F.);
#7878=ORIENTED_EDGE('',*,*,#6289,.T.);
#7879=ORIENTED_EDGE('',*,*,#6290,.F.);
#7880=ORIENTED_EDGE('',*,*,#6289,.F.);
#7881=ORIENTED_EDGE('',*,*,#6291,.F.);
#7882=ORIENTED_EDGE('',*,*,#6292,.T.);
#7883=ORIENTED_EDGE('',*,*,#6293,.F.);
#7884=ORIENTED_EDGE('',*,*,#6292,.F.);
#7885=ORIENTED_EDGE('',*,*,#6294,.F.);
#7886=ORIENTED_EDGE('',*,*,#6295,.T.);
#7887=ORIENTED_EDGE('',*,*,#6296,.F.);
#7888=ORIENTED_EDGE('',*,*,#6295,.F.);
#7889=ORIENTED_EDGE('',*,*,#6297,.F.);
#7890=ORIENTED_EDGE('',*,*,#6298,.T.);
#7891=ORIENTED_EDGE('',*,*,#6299,.F.);
#7892=ORIENTED_EDGE('',*,*,#6298,.F.);
#7893=ORIENTED_EDGE('',*,*,#6256,.F.);
#7894=ORIENTED_EDGE('',*,*,#6300,.T.);
#7895=ORIENTED_EDGE('',*,*,#6301,.F.);
#7896=ORIENTED_EDGE('',*,*,#6300,.F.);
#7897=ORIENTED_EDGE('',*,*,#6255,.F.);
#7898=ORIENTED_EDGE('',*,*,#6302,.T.);
#7899=ORIENTED_EDGE('',*,*,#6303,.F.);
#7900=ORIENTED_EDGE('',*,*,#6302,.F.);
#7901=ORIENTED_EDGE('',*,*,#6254,.F.);
#7902=ORIENTED_EDGE('',*,*,#6304,.T.);
#7903=ORIENTED_EDGE('',*,*,#6305,.F.);
#7904=ORIENTED_EDGE('',*,*,#6304,.F.);
#7905=ORIENTED_EDGE('',*,*,#6253,.F.);
#7906=ORIENTED_EDGE('',*,*,#6306,.T.);
#7907=ORIENTED_EDGE('',*,*,#6307,.F.);
#7908=ORIENTED_EDGE('',*,*,#6306,.F.);
#7909=ORIENTED_EDGE('',*,*,#6252,.F.);
#7910=ORIENTED_EDGE('',*,*,#6308,.T.);
#7911=ORIENTED_EDGE('',*,*,#6309,.F.);
#7912=ORIENTED_EDGE('',*,*,#6308,.F.);
#7913=ORIENTED_EDGE('',*,*,#6251,.F.);
#7914=ORIENTED_EDGE('',*,*,#6310,.T.);
#7915=ORIENTED_EDGE('',*,*,#6311,.F.);
#7916=ORIENTED_EDGE('',*,*,#6310,.F.);
#7917=ORIENTED_EDGE('',*,*,#6250,.F.);
#7918=ORIENTED_EDGE('',*,*,#6312,.T.);
#7919=ORIENTED_EDGE('',*,*,#6313,.F.);
#7920=ORIENTED_EDGE('',*,*,#6312,.F.);
#7921=ORIENTED_EDGE('',*,*,#6249,.F.);
#7922=ORIENTED_EDGE('',*,*,#6314,.T.);
#7923=ORIENTED_EDGE('',*,*,#6315,.F.);
#7924=ORIENTED_EDGE('',*,*,#6314,.F.);
#7925=ORIENTED_EDGE('',*,*,#6248,.F.);
#7926=ORIENTED_EDGE('',*,*,#6316,.T.);
#7927=ORIENTED_EDGE('',*,*,#6317,.F.);
#7928=ORIENTED_EDGE('',*,*,#6316,.F.);
#7929=ORIENTED_EDGE('',*,*,#6247,.F.);
#7930=ORIENTED_EDGE('',*,*,#6318,.T.);
#7931=ORIENTED_EDGE('',*,*,#6319,.F.);
#7932=ORIENTED_EDGE('',*,*,#6318,.F.);
#7933=ORIENTED_EDGE('',*,*,#6246,.F.);
#7934=ORIENTED_EDGE('',*,*,#6320,.T.);
#7935=ORIENTED_EDGE('',*,*,#6321,.F.);
#7936=ORIENTED_EDGE('',*,*,#6320,.F.);
#7937=ORIENTED_EDGE('',*,*,#6322,.F.);
#7938=ORIENTED_EDGE('',*,*,#6323,.T.);
#7939=ORIENTED_EDGE('',*,*,#6324,.F.);
#7940=ORIENTED_EDGE('',*,*,#6323,.F.);
#7941=ORIENTED_EDGE('',*,*,#6325,.F.);
#7942=ORIENTED_EDGE('',*,*,#6326,.T.);
#7943=ORIENTED_EDGE('',*,*,#6327,.F.);
#7944=ORIENTED_EDGE('',*,*,#6326,.F.);
#7945=ORIENTED_EDGE('',*,*,#6328,.F.);
#7946=ORIENTED_EDGE('',*,*,#6329,.T.);
#7947=ORIENTED_EDGE('',*,*,#6330,.F.);
#7948=ORIENTED_EDGE('',*,*,#6329,.F.);
#7949=ORIENTED_EDGE('',*,*,#6331,.F.);
#7950=ORIENTED_EDGE('',*,*,#6332,.T.);
#7951=ORIENTED_EDGE('',*,*,#6333,.F.);
#7952=ORIENTED_EDGE('',*,*,#6332,.F.);
#7953=ORIENTED_EDGE('',*,*,#6334,.F.);
#7954=ORIENTED_EDGE('',*,*,#6335,.T.);
#7955=ORIENTED_EDGE('',*,*,#6336,.F.);
#7956=ORIENTED_EDGE('',*,*,#6335,.F.);
#7957=ORIENTED_EDGE('',*,*,#6337,.F.);
#7958=ORIENTED_EDGE('',*,*,#6338,.T.);
#7959=ORIENTED_EDGE('',*,*,#6339,.F.);
#7960=ORIENTED_EDGE('',*,*,#6338,.F.);
#7961=ORIENTED_EDGE('',*,*,#6340,.F.);
#7962=ORIENTED_EDGE('',*,*,#6341,.T.);
#7963=ORIENTED_EDGE('',*,*,#6342,.F.);
#7964=ORIENTED_EDGE('',*,*,#6341,.F.);
#7965=ORIENTED_EDGE('',*,*,#6343,.F.);
#7966=ORIENTED_EDGE('',*,*,#6344,.T.);
#7967=ORIENTED_EDGE('',*,*,#6345,.F.);
#7968=ORIENTED_EDGE('',*,*,#6344,.F.);
#7969=ORIENTED_EDGE('',*,*,#6346,.F.);
#7970=ORIENTED_EDGE('',*,*,#6347,.T.);
#7971=ORIENTED_EDGE('',*,*,#6348,.F.);
#7972=ORIENTED_EDGE('',*,*,#6347,.F.);
#7973=ORIENTED_EDGE('',*,*,#6349,.F.);
#7974=ORIENTED_EDGE('',*,*,#6350,.T.);
#7975=ORIENTED_EDGE('',*,*,#6351,.F.);
#7976=ORIENTED_EDGE('',*,*,#6350,.F.);
#7977=ORIENTED_EDGE('',*,*,#6352,.F.);
#7978=ORIENTED_EDGE('',*,*,#6353,.T.);
#7979=ORIENTED_EDGE('',*,*,#6354,.F.);
#7980=ORIENTED_EDGE('',*,*,#6353,.F.);
#7981=ORIENTED_EDGE('',*,*,#6262,.F.);
#7982=ORIENTED_EDGE('',*,*,#6355,.T.);
#7983=ORIENTED_EDGE('',*,*,#6356,.F.);
#7984=ORIENTED_EDGE('',*,*,#6357,.F.);
#7985=ORIENTED_EDGE('',*,*,#6266,.F.);
#7986=ORIENTED_EDGE('',*,*,#6263,.F.);
#7987=ORIENTED_EDGE('',*,*,#6357,.T.);
#7988=ORIENTED_EDGE('',*,*,#6358,.F.);
#7989=ORIENTED_EDGE('',*,*,#6352,.T.);
#7990=ORIENTED_EDGE('',*,*,#6349,.T.);
#7991=ORIENTED_EDGE('',*,*,#6346,.T.);
#7992=ORIENTED_EDGE('',*,*,#6343,.T.);
#7993=ORIENTED_EDGE('',*,*,#6340,.T.);
#7994=ORIENTED_EDGE('',*,*,#6337,.T.);
#7995=ORIENTED_EDGE('',*,*,#6334,.T.);
#7996=ORIENTED_EDGE('',*,*,#6331,.T.);
#7997=ORIENTED_EDGE('',*,*,#6328,.T.);
#7998=ORIENTED_EDGE('',*,*,#6325,.T.);
#7999=ORIENTED_EDGE('',*,*,#6322,.T.);
#8000=ORIENTED_EDGE('',*,*,#6240,.F.);
#8001=ORIENTED_EDGE('',*,*,#6359,.F.);
#8002=ORIENTED_EDGE('',*,*,#6360,.F.);
#8003=ORIENTED_EDGE('',*,*,#6257,.F.);
#8004=ORIENTED_EDGE('',*,*,#6299,.T.);
#8005=ORIENTED_EDGE('',*,*,#6296,.T.);
#8006=ORIENTED_EDGE('',*,*,#6293,.T.);
#8007=ORIENTED_EDGE('',*,*,#6290,.T.);
#8008=ORIENTED_EDGE('',*,*,#6287,.T.);
#8009=ORIENTED_EDGE('',*,*,#6284,.T.);
#8010=ORIENTED_EDGE('',*,*,#6281,.T.);
#8011=ORIENTED_EDGE('',*,*,#6278,.T.);
#8012=ORIENTED_EDGE('',*,*,#6275,.T.);
#8013=ORIENTED_EDGE('',*,*,#6272,.T.);
#8014=ORIENTED_EDGE('',*,*,#6269,.T.);
#8015=ORIENTED_EDGE('',*,*,#6258,.F.);
#8016=ORIENTED_EDGE('',*,*,#6360,.T.);
#8017=ORIENTED_EDGE('',*,*,#6361,.F.);
#8018=ORIENTED_EDGE('',*,*,#6362,.F.);
#8019=ORIENTED_EDGE('',*,*,#6259,.T.);
#8020=ORIENTED_EDGE('',*,*,#6362,.T.);
#8021=ORIENTED_EDGE('',*,*,#6363,.F.);
#8022=ORIENTED_EDGE('',*,*,#6364,.F.);
#8023=ORIENTED_EDGE('',*,*,#6297,.T.);
#8024=ORIENTED_EDGE('',*,*,#6294,.T.);
#8025=ORIENTED_EDGE('',*,*,#6291,.T.);
#8026=ORIENTED_EDGE('',*,*,#6288,.T.);
#8027=ORIENTED_EDGE('',*,*,#6285,.T.);
#8028=ORIENTED_EDGE('',*,*,#6282,.T.);
#8029=ORIENTED_EDGE('',*,*,#6279,.T.);
#8030=ORIENTED_EDGE('',*,*,#6276,.T.);
#8031=ORIENTED_EDGE('',*,*,#6273,.T.);
#8032=ORIENTED_EDGE('',*,*,#6270,.T.);
#8033=ORIENTED_EDGE('',*,*,#6267,.T.);
#8034=ORIENTED_EDGE('',*,*,#6260,.T.);
#8035=ORIENTED_EDGE('',*,*,#6364,.T.);
#8036=ORIENTED_EDGE('',*,*,#6365,.F.);
#8037=ORIENTED_EDGE('',*,*,#6366,.F.);
#8038=ORIENTED_EDGE('',*,*,#6321,.T.);
#8039=ORIENTED_EDGE('',*,*,#6319,.T.);
#8040=ORIENTED_EDGE('',*,*,#6317,.T.);
#8041=ORIENTED_EDGE('',*,*,#6315,.T.);
#8042=ORIENTED_EDGE('',*,*,#6313,.T.);
#8043=ORIENTED_EDGE('',*,*,#6311,.T.);
#8044=ORIENTED_EDGE('',*,*,#6309,.T.);
#8045=ORIENTED_EDGE('',*,*,#6307,.T.);
#8046=ORIENTED_EDGE('',*,*,#6305,.T.);
#8047=ORIENTED_EDGE('',*,*,#6303,.T.);
#8048=ORIENTED_EDGE('',*,*,#6301,.T.);
#8049=ORIENTED_EDGE('',*,*,#6261,.T.);
#8050=ORIENTED_EDGE('',*,*,#6366,.T.);
#8051=ORIENTED_EDGE('',*,*,#6367,.F.);
#8052=ORIENTED_EDGE('',*,*,#6355,.F.);
#8053=ORIENTED_EDGE('',*,*,#6354,.T.);
#8054=ORIENTED_EDGE('',*,*,#6351,.T.);
#8055=ORIENTED_EDGE('',*,*,#6348,.T.);
#8056=ORIENTED_EDGE('',*,*,#6345,.T.);
#8057=ORIENTED_EDGE('',*,*,#6342,.T.);
#8058=ORIENTED_EDGE('',*,*,#6339,.T.);
#8059=ORIENTED_EDGE('',*,*,#6336,.T.);
#8060=ORIENTED_EDGE('',*,*,#6333,.T.);
#8061=ORIENTED_EDGE('',*,*,#6330,.T.);
#8062=ORIENTED_EDGE('',*,*,#6327,.T.);
#8063=ORIENTED_EDGE('',*,*,#6324,.T.);
#8064=ORIENTED_EDGE('',*,*,#6239,.F.);
#8065=ORIENTED_EDGE('',*,*,#6245,.T.);
#8066=ORIENTED_EDGE('',*,*,#6265,.F.);
#8067=ORIENTED_EDGE('',*,*,#6358,.T.);
#8068=ORIENTED_EDGE('',*,*,#6356,.T.);
#8069=ORIENTED_EDGE('',*,*,#6367,.T.);
#8070=ORIENTED_EDGE('',*,*,#6365,.T.);
#8071=ORIENTED_EDGE('',*,*,#6363,.T.);
#8072=ORIENTED_EDGE('',*,*,#6361,.T.);
#8073=ORIENTED_EDGE('',*,*,#6359,.T.);
#10797=ADVANCED_FACE('',(#2921),#2561,.T.);
#10798=ADVANCED_FACE('',(#2922,#118,#119,#120,#121,#122,#123,#124,#125,
#126,#127,#128),#637,.T.);
#10799=ADVANCED_FACE('',(#2923),#638,.F.);
#10800=ADVANCED_FACE('',(#2924),#2562,.T.);
#10801=ADVANCED_FACE('',(#2925),#2563,.F.);
#10802=ADVANCED_FACE('',(#2926),#2564,.F.);
#10803=ADVANCED_FACE('',(#2927),#2565,.F.);
#10804=ADVANCED_FACE('',(#2928),#2566,.F.);
#10805=ADVANCED_FACE('',(#2929),#2567,.F.);
#10806=ADVANCED_FACE('',(#2930),#2568,.F.);
#10807=ADVANCED_FACE('',(#2931),#2569,.F.);
#10808=ADVANCED_FACE('',(#2932),#2570,.F.);
#10809=ADVANCED_FACE('',(#2933),#2571,.F.);
#10810=ADVANCED_FACE('',(#2934),#2572,.F.);
#10811=ADVANCED_FACE('',(#2935),#2573,.F.);
#10812=ADVANCED_FACE('',(#2936),#2574,.F.);
#10813=ADVANCED_FACE('',(#2937),#2575,.F.);
#10814=ADVANCED_FACE('',(#2938),#2576,.F.);
#10815=ADVANCED_FACE('',(#2939),#2577,.F.);
#10816=ADVANCED_FACE('',(#2940),#2578,.F.);
#10817=ADVANCED_FACE('',(#2941),#2579,.F.);
#10818=ADVANCED_FACE('',(#2942),#2580,.F.);
#10819=ADVANCED_FACE('',(#2943),#2581,.F.);
#10820=ADVANCED_FACE('',(#2944),#2582,.F.);
#10821=ADVANCED_FACE('',(#2945),#2583,.F.);
#10822=ADVANCED_FACE('',(#2946),#2584,.F.);
#10823=ADVANCED_FACE('',(#2947),#2585,.F.);
#10824=ADVANCED_FACE('',(#2948),#2586,.F.);
#10825=ADVANCED_FACE('',(#2949),#2587,.F.);
#10826=ADVANCED_FACE('',(#2950),#2588,.F.);
#10827=ADVANCED_FACE('',(#2951),#2589,.F.);
#10828=ADVANCED_FACE('',(#2952),#2590,.F.);
#10829=ADVANCED_FACE('',(#2953),#2591,.F.);
#10830=ADVANCED_FACE('',(#2954),#2592,.F.);
#10831=ADVANCED_FACE('',(#2955),#2593,.F.);
#10832=ADVANCED_FACE('',(#2956),#2594,.F.);
#10833=ADVANCED_FACE('',(#2957),#2595,.F.);
#10834=ADVANCED_FACE('',(#2958),#639,.T.);
#10835=ADVANCED_FACE('',(#2959,#129,#130,#131,#132,#133,#134,#135,#136,
#137,#138,#139),#640,.T.);
#10836=ADVANCED_FACE('',(#2960,#140,#141,#142,#143,#144,#145,#146,#147,
#148,#149,#150),#641,.T.);
#10837=ADVANCED_FACE('',(#2961),#642,.T.);
#10838=ADVANCED_FACE('',(#2962,#151,#152,#153,#154,#155,#156,#157,#158,
#159,#160,#161),#643,.T.);
#10839=ADVANCED_FACE('',(#2963,#162,#163,#164,#165,#166,#167,#168,#169,
#170,#171,#172),#644,.T.);
#10840=ADVANCED_FACE('',(#2964,#173,#174,#175,#176,#177,#178,#179,#180,
#181,#182,#183),#645,.T.);
#10841=ADVANCED_FACE('',(#2965),#646,.T.);
#11316=CLOSED_SHELL('',(#10797,#10798,#10799,#10800,#10801,#10802,#10803,
#10804,#10805,#10806,#10807,#10808,#10809,#10810,#10811,#10812,#10813,#10814,
#10815,#10816,#10817,#10818,#10819,#10820,#10821,#10822,#10823,#10824,#10825,
#10826,#10827,#10828,#10829,#10830,#10831,#10832,#10833,#10834,#10835,#10836,
#10837,#10838,#10839,#10840,#10841));
#11555=AXIS2_PLACEMENT_3D('',#16191,#12884,#12885);
#11556=AXIS2_PLACEMENT_3D('',#16192,#12886,#12887);
#11557=AXIS2_PLACEMENT_3D('',#16195,#12888,#12889);
#11558=AXIS2_PLACEMENT_3D('',#16199,#12891,#12892);
#11559=AXIS2_PLACEMENT_3D('',#16201,#12894,#12895);
#11560=AXIS2_PLACEMENT_3D('',#16208,#12899,#12900);
#11561=AXIS2_PLACEMENT_3D('',#16210,#12901,#12902);
#11562=AXIS2_PLACEMENT_3D('',#16212,#12903,#12904);
#11563=AXIS2_PLACEMENT_3D('',#16214,#12905,#12906);
#11564=AXIS2_PLACEMENT_3D('',#16216,#12907,#12908);
#11565=AXIS2_PLACEMENT_3D('',#16218,#12909,#12910);
#11566=AXIS2_PLACEMENT_3D('',#16220,#12911,#12912);
#11567=AXIS2_PLACEMENT_3D('',#16222,#12913,#12914);
#11568=AXIS2_PLACEMENT_3D('',#16224,#12915,#12916);
#11569=AXIS2_PLACEMENT_3D('',#16226,#12917,#12918);
#11570=AXIS2_PLACEMENT_3D('',#16228,#12919,#12920);
#11571=AXIS2_PLACEMENT_3D('',#16229,#12921,#12922);
#11572=AXIS2_PLACEMENT_3D('',#16244,#12930,#12931);
#11573=AXIS2_PLACEMENT_3D('',#16245,#12932,#12933);
#11574=AXIS2_PLACEMENT_3D('',#16247,#12934,#12935);
#11575=AXIS2_PLACEMENT_3D('',#16249,#12937,#12938);
#11576=AXIS2_PLACEMENT_3D('',#16251,#12939,#12940);
#11577=AXIS2_PLACEMENT_3D('',#16254,#12942,#12943);
#11578=AXIS2_PLACEMENT_3D('',#16255,#12944,#12945);
#11579=AXIS2_PLACEMENT_3D('',#16257,#12946,#12947);
#11580=AXIS2_PLACEMENT_3D('',#16260,#12949,#12950);
#11581=AXIS2_PLACEMENT_3D('',#16261,#12951,#12952);
#11582=AXIS2_PLACEMENT_3D('',#16263,#12953,#12954);
#11583=AXIS2_PLACEMENT_3D('',#16266,#12956,#12957);
#11584=AXIS2_PLACEMENT_3D('',#16267,#12958,#12959);
#11585=AXIS2_PLACEMENT_3D('',#16269,#12960,#12961);
#11586=AXIS2_PLACEMENT_3D('',#16272,#12963,#12964);
#11587=AXIS2_PLACEMENT_3D('',#16273,#12965,#12966);
#11588=AXIS2_PLACEMENT_3D('',#16275,#12967,#12968);
#11589=AXIS2_PLACEMENT_3D('',#16278,#12970,#12971);
#11590=AXIS2_PLACEMENT_3D('',#16279,#12972,#12973);
#11591=AXIS2_PLACEMENT_3D('',#16281,#12974,#12975);
#11592=AXIS2_PLACEMENT_3D('',#16284,#12977,#12978);
#11593=AXIS2_PLACEMENT_3D('',#16285,#12979,#12980);
#11594=AXIS2_PLACEMENT_3D('',#16287,#12981,#12982);
#11595=AXIS2_PLACEMENT_3D('',#16290,#12984,#12985);
#11596=AXIS2_PLACEMENT_3D('',#16291,#12986,#12987);
#11597=AXIS2_PLACEMENT_3D('',#16293,#12988,#12989);
#11598=AXIS2_PLACEMENT_3D('',#16296,#12991,#12992);
#11599=AXIS2_PLACEMENT_3D('',#16297,#12993,#12994);
#11600=AXIS2_PLACEMENT_3D('',#16299,#12995,#12996);
#11601=AXIS2_PLACEMENT_3D('',#16302,#12998,#12999);
#11602=AXIS2_PLACEMENT_3D('',#16303,#13000,#13001);
#11603=AXIS2_PLACEMENT_3D('',#16305,#13002,#13003);
#11604=AXIS2_PLACEMENT_3D('',#16308,#13005,#13006);
#11605=AXIS2_PLACEMENT_3D('',#16309,#13007,#13008);
#11606=AXIS2_PLACEMENT_3D('',#16311,#13009,#13010);
#11607=AXIS2_PLACEMENT_3D('',#16314,#13012,#13013);
#11608=AXIS2_PLACEMENT_3D('',#16315,#13014,#13015);
#11609=AXIS2_PLACEMENT_3D('',#16318,#13017,#13018);
#11610=AXIS2_PLACEMENT_3D('',#16319,#13019,#13020);
#11611=AXIS2_PLACEMENT_3D('',#16322,#13022,#13023);
#11612=AXIS2_PLACEMENT_3D('',#16323,#13024,#13025);
#11613=AXIS2_PLACEMENT_3D('',#16326,#13027,#13028);
#11614=AXIS2_PLACEMENT_3D('',#16327,#13029,#13030);
#11615=AXIS2_PLACEMENT_3D('',#16330,#13032,#13033);
#11616=AXIS2_PLACEMENT_3D('',#16331,#13034,#13035);
#11617=AXIS2_PLACEMENT_3D('',#16334,#13037,#13038);
#11618=AXIS2_PLACEMENT_3D('',#16335,#13039,#13040);
#11619=AXIS2_PLACEMENT_3D('',#16338,#13042,#13043);
#11620=AXIS2_PLACEMENT_3D('',#16339,#13044,#13045);
#11621=AXIS2_PLACEMENT_3D('',#16342,#13047,#13048);
#11622=AXIS2_PLACEMENT_3D('',#16343,#13049,#13050);
#11623=AXIS2_PLACEMENT_3D('',#16346,#13052,#13053);
#11624=AXIS2_PLACEMENT_3D('',#16347,#13054,#13055);
#11625=AXIS2_PLACEMENT_3D('',#16350,#13057,#13058);
#11626=AXIS2_PLACEMENT_3D('',#16351,#13059,#13060);
#11627=AXIS2_PLACEMENT_3D('',#16354,#13062,#13063);
#11628=AXIS2_PLACEMENT_3D('',#16355,#13064,#13065);
#11629=AXIS2_PLACEMENT_3D('',#16358,#13067,#13068);
#11630=AXIS2_PLACEMENT_3D('',#16359,#13069,#13070);
#11631=AXIS2_PLACEMENT_3D('',#16361,#13071,#13072);
#11632=AXIS2_PLACEMENT_3D('',#16364,#13074,#13075);
#11633=AXIS2_PLACEMENT_3D('',#16365,#13076,#13077);
#11634=AXIS2_PLACEMENT_3D('',#16367,#13078,#13079);
#11635=AXIS2_PLACEMENT_3D('',#16370,#13081,#13082);
#11636=AXIS2_PLACEMENT_3D('',#16371,#13083,#13084);
#11637=AXIS2_PLACEMENT_3D('',#16373,#13085,#13086);
#11638=AXIS2_PLACEMENT_3D('',#16376,#13088,#13089);
#11639=AXIS2_PLACEMENT_3D('',#16377,#13090,#13091);
#11640=AXIS2_PLACEMENT_3D('',#16379,#13092,#13093);
#11641=AXIS2_PLACEMENT_3D('',#16382,#13095,#13096);
#11642=AXIS2_PLACEMENT_3D('',#16383,#13097,#13098);
#11643=AXIS2_PLACEMENT_3D('',#16385,#13099,#13100);
#11644=AXIS2_PLACEMENT_3D('',#16388,#13102,#13103);
#11645=AXIS2_PLACEMENT_3D('',#16389,#13104,#13105);
#11646=AXIS2_PLACEMENT_3D('',#16391,#13106,#13107);
#11647=AXIS2_PLACEMENT_3D('',#16394,#13109,#13110);
#11648=AXIS2_PLACEMENT_3D('',#16395,#13111,#13112);
#11649=AXIS2_PLACEMENT_3D('',#16397,#13113,#13114);
#11650=AXIS2_PLACEMENT_3D('',#16400,#13116,#13117);
#11651=AXIS2_PLACEMENT_3D('',#16401,#13118,#13119);
#11652=AXIS2_PLACEMENT_3D('',#16403,#13120,#13121);
#11653=AXIS2_PLACEMENT_3D('',#16406,#13123,#13124);
#11654=AXIS2_PLACEMENT_3D('',#16407,#13125,#13126);
#11655=AXIS2_PLACEMENT_3D('',#16409,#13127,#13128);
#11656=AXIS2_PLACEMENT_3D('',#16412,#13130,#13131);
#11657=AXIS2_PLACEMENT_3D('',#16413,#13132,#13133);
#11658=AXIS2_PLACEMENT_3D('',#16415,#13134,#13135);
#11659=AXIS2_PLACEMENT_3D('',#16418,#13137,#13138);
#11660=AXIS2_PLACEMENT_3D('',#16419,#13139,#13140);
#11661=AXIS2_PLACEMENT_3D('',#16421,#13141,#13142);
#11662=AXIS2_PLACEMENT_3D('',#16424,#13144,#13145);
#11663=AXIS2_PLACEMENT_3D('',#16425,#13146,#13147);
#11664=AXIS2_PLACEMENT_3D('',#16431,#13151,#13152);
#11665=AXIS2_PLACEMENT_3D('',#16433,#13154,#13155);
#11666=AXIS2_PLACEMENT_3D('',#16437,#13158,#13159);
#11667=AXIS2_PLACEMENT_3D('',#16441,#13162,#13163);
#11668=AXIS2_PLACEMENT_3D('',#16445,#13166,#13167);
#11669=AXIS2_PLACEMENT_3D('',#16449,#13170,#13171);
#11670=AXIS2_PLACEMENT_3D('',#16451,#13173,#13174);
#12884=DIRECTION('axis',(0.,0.,1.));
#12885=DIRECTION('refdir',(1.,0.,0.));
#12886=DIRECTION('center_axis',(0.,1.,0.));
#12887=DIRECTION('ref_axis',(-0.707106781186548,0.,-0.707106781186548));
#12888=DIRECTION('center_axis',(0.,-1.,0.));
#12889=DIRECTION('ref_axis',(-0.707106781186548,0.,-0.707106781186548));
#12890=DIRECTION('',(0.,-1.,0.));
#12891=DIRECTION('center_axis',(0.,1.,0.));
#12892=DIRECTION('ref_axis',(-0.707106781186548,0.,-0.707106781186548));
#12893=DIRECTION('',(0.,1.,0.));
#12894=DIRECTION('center_axis',(-1.,0.,0.));
#12895=DIRECTION('ref_axis',(0.,0.,1.));
#12896=DIRECTION('',(0.,0.,-1.));
#12897=DIRECTION('',(0.,-1.,0.));
#12898=DIRECTION('',(0.,0.,1.));
#12899=DIRECTION('center_axis',(1.,0.,0.));
#12900=DIRECTION('ref_axis',(2.22044604925031E-16,0.,1.));
#12901=DIRECTION('center_axis',(1.,0.,0.));
#12902=DIRECTION('ref_axis',(2.22044604925031E-16,0.,1.));
#12903=DIRECTION('center_axis',(1.,0.,0.));
#12904=DIRECTION('ref_axis',(2.22044604925031E-16,0.,1.));
#12905=DIRECTION('center_axis',(1.,0.,0.));
#12906=DIRECTION('ref_axis',(2.22044604925031E-16,0.,1.));
#12907=DIRECTION('center_axis',(1.,0.,0.));
#12908=DIRECTION('ref_axis',(2.22044604925031E-16,0.,1.));
#12909=DIRECTION('center_axis',(1.,0.,0.));
#12910=DIRECTION('ref_axis',(2.22044604925031E-16,0.,1.));
#12911=DIRECTION('center_axis',(1.,0.,0.));
#12912=DIRECTION('ref_axis',(2.22044604925031E-16,0.,1.));
#12913=DIRECTION('center_axis',(1.,0.,0.));
#12914=DIRECTION('ref_axis',(2.22044604925031E-16,0.,1.));
#12915=DIRECTION('center_axis',(1.,0.,0.));
#12916=DIRECTION('ref_axis',(2.22044604925031E-16,0.,1.));
#12917=DIRECTION('center_axis',(1.,0.,0.));
#12918=DIRECTION('ref_axis',(2.22044604925031E-16,0.,1.));
#12919=DIRECTION('center_axis',(1.,0.,0.));
#12920=DIRECTION('ref_axis',(2.22044604925031E-16,0.,1.));
#12921=DIRECTION('center_axis',(0.,1.,0.));
#12922=DIRECTION('ref_axis',(1.,0.,0.));
#12923=DIRECTION('',(1.,0.,0.));
#12924=DIRECTION('',(0.,0.,1.));
#12925=DIRECTION('',(1.,0.,4.89653224666665E-17));
#12926=DIRECTION('',(5.18929031489969E-17,0.,-1.));
#12927=DIRECTION('',(-1.,0.,0.));
#12928=DIRECTION('',(0.,0.,1.));
#12929=DIRECTION('',(-1.,0.,0.));
#12930=DIRECTION('center_axis',(0.,1.,0.));
#12931=DIRECTION('ref_axis',(-0.707106781186549,0.,0.707106781186546));
#12932=DIRECTION('center_axis',(0.,1.,0.));
#12933=DIRECTION('ref_axis',(-0.707106781186549,0.,0.707106781186546));
#12934=DIRECTION('center_axis',(0.,-1.,0.));
#12935=DIRECTION('ref_axis',(-0.707106781186549,0.,0.707106781186546));
#12936=DIRECTION('',(0.,1.,0.));
#12937=DIRECTION('center_axis',(0.,0.,-1.));
#12938=DIRECTION('ref_axis',(-1.,0.,0.));
#12939=DIRECTION('center_axis',(4.89653224666665E-17,0.,-1.));
#12940=DIRECTION('ref_axis',(-1.,0.,0.));
#12941=DIRECTION('',(0.,0.,-1.));
#12942=DIRECTION('center_axis',(0.,0.,1.));
#12943=DIRECTION('ref_axis',(-1.,0.,0.));
#12944=DIRECTION('center_axis',(0.,0.,-1.));
#12945=DIRECTION('ref_axis',(-1.,0.,0.));
#12946=DIRECTION('center_axis',(4.89653224666665E-17,0.,-1.));
#12947=DIRECTION('ref_axis',(-1.,0.,0.));
#12948=DIRECTION('',(0.,0.,-1.));
#12949=DIRECTION('center_axis',(0.,0.,1.));
#12950=DIRECTION('ref_axis',(-1.,0.,0.));
#12951=DIRECTION('center_axis',(0.,0.,-1.));
#12952=DIRECTION('ref_axis',(-1.,0.,0.));
#12953=DIRECTION('center_axis',(4.89653224666665E-17,0.,-1.));
#12954=DIRECTION('ref_axis',(-1.,0.,0.));
#12955=DIRECTION('',(0.,0.,-1.));
#12956=DIRECTION('center_axis',(0.,0.,1.));
#12957=DIRECTION('ref_axis',(-1.,0.,0.));
#12958=DIRECTION('center_axis',(0.,0.,-1.));
#12959=DIRECTION('ref_axis',(-1.,0.,0.));
#12960=DIRECTION('center_axis',(4.89653224666665E-17,0.,-1.));
#12961=DIRECTION('ref_axis',(-1.,0.,0.));
#12962=DIRECTION('',(0.,0.,-1.));
#12963=DIRECTION('center_axis',(0.,0.,1.));
#12964=DIRECTION('ref_axis',(-1.,0.,0.));
#12965=DIRECTION('center_axis',(0.,0.,-1.));
#12966=DIRECTION('ref_axis',(-1.,0.,0.));
#12967=DIRECTION('center_axis',(4.89653224666665E-17,0.,-1.));
#12968=DIRECTION('ref_axis',(-1.,0.,0.));
#12969=DIRECTION('',(0.,0.,-1.));
#12970=DIRECTION('center_axis',(0.,0.,1.));
#12971=DIRECTION('ref_axis',(-1.,0.,0.));
#12972=DIRECTION('center_axis',(0.,0.,-1.));
#12973=DIRECTION('ref_axis',(-1.,0.,0.));
#12974=DIRECTION('center_axis',(4.89653224666665E-17,0.,-1.));
#12975=DIRECTION('ref_axis',(-1.,0.,0.));
#12976=DIRECTION('',(0.,0.,-1.));
#12977=DIRECTION('center_axis',(0.,0.,1.));
#12978=DIRECTION('ref_axis',(-1.,0.,0.));
#12979=DIRECTION('center_axis',(0.,0.,-1.));
#12980=DIRECTION('ref_axis',(-1.,0.,0.));
#12981=DIRECTION('center_axis',(4.89653224666665E-17,0.,-1.));
#12982=DIRECTION('ref_axis',(-1.,0.,0.));
#12983=DIRECTION('',(0.,0.,-1.));
#12984=DIRECTION('center_axis',(0.,0.,1.));
#12985=DIRECTION('ref_axis',(-1.,0.,0.));
#12986=DIRECTION('center_axis',(0.,0.,-1.));
#12987=DIRECTION('ref_axis',(-1.,0.,0.));
#12988=DIRECTION('center_axis',(4.89653224666665E-17,0.,-1.));
#12989=DIRECTION('ref_axis',(-1.,0.,0.));
#12990=DIRECTION('',(0.,0.,-1.));
#12991=DIRECTION('center_axis',(0.,0.,1.));
#12992=DIRECTION('ref_axis',(-1.,0.,0.));
#12993=DIRECTION('center_axis',(0.,0.,-1.));
#12994=DIRECTION('ref_axis',(-1.,0.,0.));
#12995=DIRECTION('center_axis',(4.89653224666665E-17,0.,-1.));
#12996=DIRECTION('ref_axis',(-1.,0.,0.));
#12997=DIRECTION('',(0.,0.,-1.));
#12998=DIRECTION('center_axis',(0.,0.,1.));
#12999=DIRECTION('ref_axis',(-1.,0.,0.));
#13000=DIRECTION('center_axis',(0.,0.,-1.));
#13001=DIRECTION('ref_axis',(-1.,0.,0.));
#13002=DIRECTION('center_axis',(4.89653224666665E-17,0.,-1.));
#13003=DIRECTION('ref_axis',(-1.,0.,0.));
#13004=DIRECTION('',(0.,0.,-1.));
#13005=DIRECTION('center_axis',(0.,0.,1.));
#13006=DIRECTION('ref_axis',(-1.,0.,0.));
#13007=DIRECTION('center_axis',(0.,0.,-1.));
#13008=DIRECTION('ref_axis',(-1.,0.,0.));
#13009=DIRECTION('center_axis',(4.89653224666665E-17,0.,-1.));
#13010=DIRECTION('ref_axis',(-1.,0.,0.));
#13011=DIRECTION('',(0.,0.,-1.));
#13012=DIRECTION('center_axis',(0.,0.,1.));
#13013=DIRECTION('ref_axis',(-1.,0.,0.));
#13014=DIRECTION('center_axis',(-1.,0.,-2.22044604925031E-16));
#13015=DIRECTION('ref_axis',(2.22044604925031E-16,0.,1.));
#13016=DIRECTION('',(1.,0.,2.22044604925031E-16));
#13017=DIRECTION('center_axis',(-1.,0.,-5.18929031489969E-17));
#13018=DIRECTION('ref_axis',(2.22044604925031E-16,0.,1.));
#13019=DIRECTION('center_axis',(-1.,0.,-2.22044604925031E-16));
#13020=DIRECTION('ref_axis',(2.22044604925031E-16,0.,1.));
#13021=DIRECTION('',(1.,0.,2.22044604925031E-16));
#13022=DIRECTION('center_axis',(-1.,0.,-5.18929031489969E-17));
#13023=DIRECTION('ref_axis',(2.22044604925031E-16,0.,1.));
#13024=DIRECTION('center_axis',(-1.,0.,-2.22044604925031E-16));
#13025=DIRECTION('ref_axis',(2.22044604925031E-16,0.,1.));
#13026=DIRECTION('',(1.,0.,2.22044604925031E-16));
#13027=DIRECTION('center_axis',(-1.,0.,-5.18929031489969E-17));
#13028=DIRECTION('ref_axis',(2.22044604925031E-16,0.,1.));
#13029=DIRECTION('center_axis',(-1.,0.,-2.22044604925031E-16));
#13030=DIRECTION('ref_axis',(2.22044604925031E-16,0.,1.));
#13031=DIRECTION('',(1.,0.,2.22044604925031E-16));
#13032=DIRECTION('center_axis',(-1.,0.,-5.18929031489969E-17));
#13033=DIRECTION('ref_axis',(2.22044604925031E-16,0.,1.));
#13034=DIRECTION('center_axis',(-1.,0.,-2.22044604925031E-16));
#13035=DIRECTION('ref_axis',(2.22044604925031E-16,0.,1.));
#13036=DIRECTION('',(1.,0.,2.22044604925031E-16));
#13037=DIRECTION('center_axis',(-1.,0.,-5.18929031489969E-17));
#13038=DIRECTION('ref_axis',(2.22044604925031E-16,0.,1.));
#13039=DIRECTION('center_axis',(-1.,0.,-2.22044604925031E-16));
#13040=DIRECTION('ref_axis',(2.22044604925031E-16,0.,1.));
#13041=DIRECTION('',(1.,0.,2.22044604925031E-16));
#13042=DIRECTION('center_axis',(-1.,0.,-5.18929031489969E-17));
#13043=DIRECTION('ref_axis',(2.22044604925031E-16,0.,1.));
#13044=DIRECTION('center_axis',(-1.,0.,-2.22044604925031E-16));
#13045=DIRECTION('ref_axis',(2.22044604925031E-16,0.,1.));
#13046=DIRECTION('',(1.,0.,2.22044604925031E-16));
#13047=DIRECTION('center_axis',(-1.,0.,-5.18929031489969E-17));
#13048=DIRECTION('ref_axis',(2.22044604925031E-16,0.,1.));
#13049=DIRECTION('center_axis',(-1.,0.,-2.22044604925031E-16));
#13050=DIRECTION('ref_axis',(2.22044604925031E-16,0.,1.));
#13051=DIRECTION('',(1.,0.,2.22044604925031E-16));
#13052=DIRECTION('center_axis',(-1.,0.,-5.18929031489969E-17));
#13053=DIRECTION('ref_axis',(2.22044604925031E-16,0.,1.));
#13054=DIRECTION('center_axis',(-1.,0.,-2.22044604925031E-16));
#13055=DIRECTION('ref_axis',(2.22044604925031E-16,0.,1.));
#13056=DIRECTION('',(1.,0.,2.22044604925031E-16));
#13057=DIRECTION('center_axis',(-1.,0.,-5.18929031489969E-17));
#13058=DIRECTION('ref_axis',(2.22044604925031E-16,0.,1.));
#13059=DIRECTION('center_axis',(-1.,0.,-2.22044604925031E-16));
#13060=DIRECTION('ref_axis',(2.22044604925031E-16,0.,1.));
#13061=DIRECTION('',(1.,0.,2.22044604925031E-16));
#13062=DIRECTION('center_axis',(-1.,0.,-5.18929031489969E-17));
#13063=DIRECTION('ref_axis',(2.22044604925031E-16,0.,1.));
#13064=DIRECTION('center_axis',(-1.,0.,-2.22044604925031E-16));
#13065=DIRECTION('ref_axis',(2.22044604925031E-16,0.,1.));
#13066=DIRECTION('',(1.,0.,2.22044604925031E-16));
#13067=DIRECTION('center_axis',(-1.,0.,-5.18929031489969E-17));
#13068=DIRECTION('ref_axis',(2.22044604925031E-16,0.,1.));
#13069=DIRECTION('center_axis',(0.,0.,-1.));
#13070=DIRECTION('ref_axis',(-1.,0.,0.));
#13071=DIRECTION('center_axis',(0.,0.,-1.));
#13072=DIRECTION('ref_axis',(-1.,0.,0.));
#13073=DIRECTION('',(0.,0.,-1.));
#13074=DIRECTION('center_axis',(0.,0.,1.));
#13075=DIRECTION('ref_axis',(-1.,0.,0.));
#13076=DIRECTION('center_axis',(0.,0.,-1.));
#13077=DIRECTION('ref_axis',(-1.,0.,0.));
#13078=DIRECTION('center_axis',(0.,0.,-1.));
#13079=DIRECTION('ref_axis',(-1.,0.,0.));
#13080=DIRECTION('',(0.,0.,-1.));
#13081=DIRECTION('center_axis',(0.,0.,1.));
#13082=DIRECTION('ref_axis',(-1.,0.,0.));
#13083=DIRECTION('center_axis',(0.,0.,-1.));
#13084=DIRECTION('ref_axis',(-1.,0.,0.));
#13085=DIRECTION('center_axis',(0.,0.,-1.));
#13086=DIRECTION('ref_axis',(-1.,0.,0.));
#13087=DIRECTION('',(0.,0.,-1.));
#13088=DIRECTION('center_axis',(0.,0.,1.));
#13089=DIRECTION('ref_axis',(-1.,0.,0.));
#13090=DIRECTION('center_axis',(0.,0.,-1.));
#13091=DIRECTION('ref_axis',(-1.,0.,0.));
#13092=DIRECTION('center_axis',(0.,0.,-1.));
#13093=DIRECTION('ref_axis',(-1.,0.,0.));
#13094=DIRECTION('',(0.,0.,-1.));
#13095=DIRECTION('center_axis',(0.,0.,1.));
#13096=DIRECTION('ref_axis',(-1.,0.,0.));
#13097=DIRECTION('center_axis',(0.,0.,-1.));
#13098=DIRECTION('ref_axis',(-1.,0.,0.));
#13099=DIRECTION('center_axis',(0.,0.,-1.));
#13100=DIRECTION('ref_axis',(-1.,0.,0.));
#13101=DIRECTION('',(0.,0.,-1.));
#13102=DIRECTION('center_axis',(0.,0.,1.));
#13103=DIRECTION('ref_axis',(-1.,0.,0.));
#13104=DIRECTION('center_axis',(0.,0.,-1.));
#13105=DIRECTION('ref_axis',(-1.,0.,0.));
#13106=DIRECTION('center_axis',(0.,0.,-1.));
#13107=DIRECTION('ref_axis',(-1.,0.,0.));
#13108=DIRECTION('',(0.,0.,-1.));
#13109=DIRECTION('center_axis',(0.,0.,1.));
#13110=DIRECTION('ref_axis',(-1.,0.,0.));
#13111=DIRECTION('center_axis',(0.,0.,-1.));
#13112=DIRECTION('ref_axis',(-1.,0.,0.));
#13113=DIRECTION('center_axis',(0.,0.,-1.));
#13114=DIRECTION('ref_axis',(-1.,0.,0.));
#13115=DIRECTION('',(0.,0.,-1.));
#13116=DIRECTION('center_axis',(0.,0.,1.));
#13117=DIRECTION('ref_axis',(-1.,0.,0.));
#13118=DIRECTION('center_axis',(0.,0.,-1.));
#13119=DIRECTION('ref_axis',(-1.,0.,0.));
#13120=DIRECTION('center_axis',(0.,0.,-1.));
#13121=DIRECTION('ref_axis',(-1.,0.,0.));
#13122=DIRECTION('',(0.,0.,-1.));
#13123=DIRECTION('center_axis',(0.,0.,1.));
#13124=DIRECTION('ref_axis',(-1.,0.,0.));
#13125=DIRECTION('center_axis',(0.,0.,-1.));
#13126=DIRECTION('ref_axis',(-1.,0.,0.));
#13127=DIRECTION('center_axis',(0.,0.,-1.));
#13128=DIRECTION('ref_axis',(-1.,0.,0.));
#13129=DIRECTION('',(0.,0.,-1.));
#13130=DIRECTION('center_axis',(0.,0.,1.));
#13131=DIRECTION('ref_axis',(-1.,0.,0.));
#13132=DIRECTION('center_axis',(0.,0.,-1.));
#13133=DIRECTION('ref_axis',(-1.,0.,0.));
#13134=DIRECTION('center_axis',(0.,0.,-1.));
#13135=DIRECTION('ref_axis',(-1.,0.,0.));
#13136=DIRECTION('',(0.,0.,-1.));
#13137=DIRECTION('center_axis',(0.,0.,1.));
#13138=DIRECTION('ref_axis',(-1.,0.,0.));
#13139=DIRECTION('center_axis',(0.,0.,-1.));
#13140=DIRECTION('ref_axis',(-1.,0.,0.));
#13141=DIRECTION('center_axis',(0.,0.,-1.));
#13142=DIRECTION('ref_axis',(-1.,0.,0.));
#13143=DIRECTION('',(0.,0.,-1.));
#13144=DIRECTION('center_axis',(0.,0.,1.));
#13145=DIRECTION('ref_axis',(-1.,0.,0.));
#13146=DIRECTION('center_axis',(1.,0.,0.));
#13147=DIRECTION('ref_axis',(0.,0.,-1.));
#13148=DIRECTION('',(0.,1.,0.));
#13149=DIRECTION('',(0.,0.,-1.));
#13150=DIRECTION('',(0.,1.,0.));
#13151=DIRECTION('center_axis',(0.,0.,1.));
#13152=DIRECTION('ref_axis',(1.,0.,0.));
#13153=DIRECTION('',(1.,0.,0.));
#13154=DIRECTION('center_axis',(0.,0.,-1.));
#13155=DIRECTION('ref_axis',(-1.,0.,0.));
#13156=DIRECTION('',(-1.,0.,0.));
#13157=DIRECTION('',(0.,1.,0.));
#13158=DIRECTION('center_axis',(1.,0.,0.));
#13159=DIRECTION('ref_axis',(0.,0.,-1.));
#13160=DIRECTION('',(0.,0.,-1.));
#13161=DIRECTION('',(0.,1.,0.));
#13162=DIRECTION('center_axis',(-4.89653224666665E-17,0.,1.));
#13163=DIRECTION('ref_axis',(1.,0.,4.89653224666665E-17));
#13164=DIRECTION('',(1.,0.,4.89653224666665E-17));
#13165=DIRECTION('',(0.,1.,0.));
#13166=DIRECTION('center_axis',(1.,0.,5.18929031489969E-17));
#13167=DIRECTION('ref_axis',(5.18929031489969E-17,0.,-1.));
#13168=DIRECTION('',(5.18929031489969E-17,0.,-1.));
#13169=DIRECTION('',(0.,1.,0.));
#13170=DIRECTION('center_axis',(0.,0.,-1.));
#13171=DIRECTION('ref_axis',(-1.,0.,0.));
#13172=DIRECTION('',(-1.,0.,0.));
#13173=DIRECTION('center_axis',(0.,1.,0.));
#13174=DIRECTION('ref_axis',(0.,0.,1.));
#16191=CARTESIAN_POINT('',(0.,0.,0.));
#16192=CARTESIAN_POINT('Origin',(1.,0.,13.));
#16193=CARTESIAN_POINT('',(0.,50.,13.));
#16194=CARTESIAN_POINT('',(1.,50.,12.));
#16195=CARTESIAN_POINT('Origin',(1.,50.,13.));
#16196=CARTESIAN_POINT('',(1.,0.,12.));
#16197=CARTESIAN_POINT('',(1.,0.,12.));
#16198=CARTESIAN_POINT('',(0.,0.,13.));
#16199=CARTESIAN_POINT('Origin',(1.,0.,13.));
#16200=CARTESIAN_POINT('',(0.,0.,13.));
#16201=CARTESIAN_POINT('Origin',(0.,0.,12.));
#16202=CARTESIAN_POINT('',(0.,0.,58.9890118784622));
#16203=CARTESIAN_POINT('',(0.,0.,59.9890118784622));
#16204=CARTESIAN_POINT('',(0.,50.,58.9890118784622));
#16205=CARTESIAN_POINT('',(0.,0.,58.9890118784622));
#16206=CARTESIAN_POINT('',(0.,50.,59.9890118784622));
#16207=CARTESIAN_POINT('',(0.,30.9806853933445,48.4577900798939));
#16208=CARTESIAN_POINT('Origin',(-8.65036710704234E-15,30.9806853933445,
50.9577900798939));
#16209=CARTESIAN_POINT('',(-8.88178419700125E-15,30.9806853933445,17.4577900798938));
#16210=CARTESIAN_POINT('Origin',(-1.76698435436636E-15,30.9806853933445,
19.9577900798938));
#16211=CARTESIAN_POINT('',(-8.88178419700125E-15,42.6473520600112,32.9577900798939));
#16212=CARTESIAN_POINT('Origin',(-5.20867573070435E-15,42.6473520600112,
35.4577900798939));
#16213=CARTESIAN_POINT('',(-8.88178419700125E-15,25.,28.515352874563));
#16214=CARTESIAN_POINT('Origin',(-5.33247954116756E-15,25.,36.015352874563));
#16215=CARTESIAN_POINT('',(0.,7.64735206001121,48.4577900798939));
#16216=CARTESIAN_POINT('Origin',(-8.65036710704234E-15,7.64735206001121,
50.9577900798939));
#16217=CARTESIAN_POINT('',(-8.88178419700125E-15,7.64735206001121,17.4577900798938));
#16218=CARTESIAN_POINT('Origin',(-1.76698435436636E-15,7.64735206001121,
19.9577900798938));
#16219=CARTESIAN_POINT('',(-8.88178419700125E-15,7.64735206001121,32.9577900798939));
#16220=CARTESIAN_POINT('Origin',(-5.20867573070435E-15,7.64735206001121,
35.4577900798939));
#16221=CARTESIAN_POINT('',(0.,42.6473520600112,48.4577900798939));
#16222=CARTESIAN_POINT('Origin',(-8.65036710704234E-15,42.6473520600112,
50.9577900798939));
#16223=CARTESIAN_POINT('',(-8.88178419700125E-15,42.6473520600112,17.4577900798938));
#16224=CARTESIAN_POINT('Origin',(-1.76698435436636E-15,42.6473520600112,
19.9577900798938));
#16225=CARTESIAN_POINT('',(0.,19.3140187266779,48.4577900798939));
#16226=CARTESIAN_POINT('Origin',(-8.65036710704234E-15,19.3140187266779,
50.9577900798939));
#16227=CARTESIAN_POINT('',(-8.88178419700125E-15,19.3140187266779,17.4577900798938));
#16228=CARTESIAN_POINT('Origin',(-1.76698435436636E-15,19.3140187266779,
19.9577900798938));
#16229=CARTESIAN_POINT('Origin',(23.9736590038991,0.,35.9945059392311));
#16230=CARTESIAN_POINT('',(47.9473180077982,0.,12.));
#16231=CARTESIAN_POINT('',(0.,0.,12.));
#16232=CARTESIAN_POINT('',(47.9473180077982,0.,14.6));
#16233=CARTESIAN_POINT('',(47.9473180077982,0.,12.));
#16234=CARTESIAN_POINT('',(2.6,0.,14.6));
#16235=CARTESIAN_POINT('',(2.6,0.,14.6));
#16236=CARTESIAN_POINT('',(2.6,0.,57.3890118784622));
#16237=CARTESIAN_POINT('',(2.6,0.,57.3890118784622));
#16238=CARTESIAN_POINT('',(47.9473180077982,0.,57.3890118784622));
#16239=CARTESIAN_POINT('',(47.9473180077982,0.,57.3890118784622));
#16240=CARTESIAN_POINT('',(47.9473180077982,0.,59.9890118784622));
#16241=CARTESIAN_POINT('',(47.9473180077982,0.,12.));
#16242=CARTESIAN_POINT('',(0.999999999999996,0.,59.9890118784622));
#16243=CARTESIAN_POINT('',(47.9473180077982,0.,59.9890118784622));
#16244=CARTESIAN_POINT('Origin',(1.,0.,58.9890118784622));
#16245=CARTESIAN_POINT('Origin',(1.,0.,58.9890118784622));
#16246=CARTESIAN_POINT('',(0.999999999999996,50.,59.9890118784622));
#16247=CARTESIAN_POINT('Origin',(1.,50.,58.9890118784622));
#16248=CARTESIAN_POINT('',(1.,0.,59.9890118784622));
#16249=CARTESIAN_POINT('Origin',(9.03122179856829,19.3140187266779,59.9890118784622));
#16250=CARTESIAN_POINT('',(11.5312217985683,19.3140187266779,14.6));
#16251=CARTESIAN_POINT('Origin',(9.03122179856829,19.3140187266779,14.6));
#16252=CARTESIAN_POINT('',(11.5312217985683,19.3140187266779,12.));
#16253=CARTESIAN_POINT('',(11.5312217985683,19.3140187266779,59.9890118784622));
#16254=CARTESIAN_POINT('Origin',(9.03122179856829,19.3140187266779,12.));
#16255=CARTESIAN_POINT('Origin',(9.03122179856829,30.9806853933445,59.9890118784622));
#16256=CARTESIAN_POINT('',(11.5312217985683,30.9806853933445,14.6));
#16257=CARTESIAN_POINT('Origin',(9.03122179856829,30.9806853933445,14.6));
#16258=CARTESIAN_POINT('',(11.5312217985683,30.9806853933445,12.));
#16259=CARTESIAN_POINT('',(11.5312217985683,30.9806853933445,59.9890118784622));
#16260=CARTESIAN_POINT('Origin',(9.03122179856829,30.9806853933445,12.));
#16261=CARTESIAN_POINT('Origin',(9.03122179856829,42.6473520600112,59.9890118784622));
#16262=CARTESIAN_POINT('',(11.5312217985683,42.6473520600112,14.6));
#16263=CARTESIAN_POINT('Origin',(9.03122179856829,42.6473520600112,14.6));
#16264=CARTESIAN_POINT('',(11.5312217985683,42.6473520600112,12.));
#16265=CARTESIAN_POINT('',(11.5312217985683,42.6473520600112,59.9890118784622));
#16266=CARTESIAN_POINT('Origin',(9.03122179856829,42.6473520600112,12.));
#16267=CARTESIAN_POINT('Origin',(23.9736590038991,25.,59.9890118784622));
#16268=CARTESIAN_POINT('',(31.4736590038991,25.,14.6));
#16269=CARTESIAN_POINT('Origin',(23.9736590038991,25.,14.6));
#16270=CARTESIAN_POINT('',(31.4736590038991,25.,12.));
#16271=CARTESIAN_POINT('',(31.4736590038991,25.,59.9890118784622));
#16272=CARTESIAN_POINT('Origin',(23.9736590038991,25.,12.));
#16273=CARTESIAN_POINT('Origin',(40.0312217985683,30.9806853933445,59.9890118784622));
#16274=CARTESIAN_POINT('',(42.5312217985683,30.9806853933445,14.6));
#16275=CARTESIAN_POINT('Origin',(40.0312217985683,30.9806853933445,14.6));
#16276=CARTESIAN_POINT('',(42.5312217985683,30.9806853933445,12.));
#16277=CARTESIAN_POINT('',(42.5312217985683,30.9806853933445,59.9890118784622));
#16278=CARTESIAN_POINT('Origin',(40.0312217985683,30.9806853933445,12.));
#16279=CARTESIAN_POINT('Origin',(40.0312217985683,19.3140187266779,59.9890118784622));
#16280=CARTESIAN_POINT('',(42.5312217985683,19.3140187266779,14.6));
#16281=CARTESIAN_POINT('Origin',(40.0312217985683,19.3140187266779,14.6));
#16282=CARTESIAN_POINT('',(42.5312217985683,19.3140187266779,12.));
#16283=CARTESIAN_POINT('',(42.5312217985683,19.3140187266779,59.9890118784622));
#16284=CARTESIAN_POINT('Origin',(40.0312217985683,19.3140187266779,12.));
#16285=CARTESIAN_POINT('Origin',(40.0312217985683,7.64735206001121,59.9890118784622));
#16286=CARTESIAN_POINT('',(42.5312217985683,7.64735206001121,14.6));
#16287=CARTESIAN_POINT('Origin',(40.0312217985683,7.64735206001121,14.6));
#16288=CARTESIAN_POINT('',(42.5312217985683,7.64735206001121,12.));
#16289=CARTESIAN_POINT('',(42.5312217985683,7.64735206001121,59.9890118784622));
#16290=CARTESIAN_POINT('Origin',(40.0312217985683,7.64735206001121,12.));
#16291=CARTESIAN_POINT('Origin',(24.5312217985683,42.6473520600112,59.9890118784622));
#16292=CARTESIAN_POINT('',(27.0312217985683,42.6473520600112,14.6));
#16293=CARTESIAN_POINT('Origin',(24.5312217985683,42.6473520600112,14.6));
#16294=CARTESIAN_POINT('',(27.0312217985683,42.6473520600112,12.));
#16295=CARTESIAN_POINT('',(27.0312217985683,42.6473520600112,59.9890118784622));
#16296=CARTESIAN_POINT('Origin',(24.5312217985683,42.6473520600112,12.));
#16297=CARTESIAN_POINT('Origin',(40.0312217985683,42.6473520600112,59.9890118784622));
#16298=CARTESIAN_POINT('',(42.5312217985683,42.6473520600112,14.6));
#16299=CARTESIAN_POINT('Origin',(40.0312217985683,42.6473520600112,14.6));
#16300=CARTESIAN_POINT('',(42.5312217985683,42.6473520600112,12.));
#16301=CARTESIAN_POINT('',(42.5312217985683,42.6473520600112,59.9890118784622));
#16302=CARTESIAN_POINT('Origin',(40.0312217985683,42.6473520600112,12.));
#16303=CARTESIAN_POINT('Origin',(24.5312217985683,7.64735206001121,59.9890118784622));
#16304=CARTESIAN_POINT('',(27.0312217985683,7.64735206001121,14.6));
#16305=CARTESIAN_POINT('Origin',(24.5312217985683,7.64735206001121,14.6));
#16306=CARTESIAN_POINT('',(27.0312217985683,7.64735206001121,12.));
#16307=CARTESIAN_POINT('',(27.0312217985683,7.64735206001121,59.9890118784622));
#16308=CARTESIAN_POINT('Origin',(24.5312217985683,7.64735206001121,12.));
#16309=CARTESIAN_POINT('Origin',(9.03122179856829,7.64735206001121,59.9890118784622));
#16310=CARTESIAN_POINT('',(11.5312217985683,7.64735206001121,14.6));
#16311=CARTESIAN_POINT('Origin',(9.03122179856829,7.64735206001121,14.6));
#16312=CARTESIAN_POINT('',(11.5312217985683,7.64735206001121,12.));
#16313=CARTESIAN_POINT('',(11.5312217985683,7.64735206001121,59.9890118784622));
#16314=CARTESIAN_POINT('Origin',(9.03122179856829,7.64735206001121,12.));
#16315=CARTESIAN_POINT('Origin',(-8.88178419700125E-15,19.3140187266779,
19.9577900798938));
#16316=CARTESIAN_POINT('',(2.60000000000001,19.3140187266779,17.4577900798939));
#16317=CARTESIAN_POINT('',(-9.43689570931383E-15,19.3140187266779,17.4577900798939));
#16318=CARTESIAN_POINT('Origin',(2.60000000000001,19.3140187266779,19.9577900798938));
#16319=CARTESIAN_POINT('Origin',(0.,19.3140187266779,50.9577900798939));
#16320=CARTESIAN_POINT('',(2.6,19.3140187266779,48.4577900798939));
#16321=CARTESIAN_POINT('',(-5.55111512312577E-16,19.3140187266779,48.4577900798939));
#16322=CARTESIAN_POINT('Origin',(2.6,19.3140187266779,50.9577900798939));
#16323=CARTESIAN_POINT('Origin',(-8.88178419700125E-15,42.6473520600112,
19.9577900798938));
#16324=CARTESIAN_POINT('',(2.60000000000001,42.6473520600112,17.4577900798939));
#16325=CARTESIAN_POINT('',(-9.43689570931383E-15,42.6473520600112,17.4577900798939));
#16326=CARTESIAN_POINT('Origin',(2.60000000000001,42.6473520600112,19.9577900798938));
#16327=CARTESIAN_POINT('Origin',(0.,42.6473520600112,50.9577900798939));
#16328=CARTESIAN_POINT('',(2.6,42.6473520600112,48.4577900798939));
#16329=CARTESIAN_POINT('',(-5.55111512312577E-16,42.6473520600112,48.4577900798939));
#16330=CARTESIAN_POINT('Origin',(2.6,42.6473520600112,50.9577900798939));
#16331=CARTESIAN_POINT('Origin',(-8.88178419700125E-15,7.64735206001121,
35.4577900798939));
#16332=CARTESIAN_POINT('',(2.6,7.64735206001121,32.9577900798939));
#16333=CARTESIAN_POINT('',(-9.43689570931383E-15,7.64735206001121,32.9577900798939));
#16334=CARTESIAN_POINT('Origin',(2.6,7.64735206001121,35.4577900798939));
#16335=CARTESIAN_POINT('Origin',(-8.88178419700125E-15,7.64735206001121,
19.9577900798938));
#16336=CARTESIAN_POINT('',(2.60000000000001,7.64735206001121,17.4577900798939));
#16337=CARTESIAN_POINT('',(-9.43689570931383E-15,7.64735206001121,17.4577900798939));
#16338=CARTESIAN_POINT('Origin',(2.60000000000001,7.64735206001121,19.9577900798938));
#16339=CARTESIAN_POINT('Origin',(0.,7.64735206001121,50.9577900798939));
#16340=CARTESIAN_POINT('',(2.6,7.64735206001121,48.4577900798939));
#16341=CARTESIAN_POINT('',(-5.55111512312577E-16,7.64735206001121,48.4577900798939));
#16342=CARTESIAN_POINT('Origin',(2.6,7.64735206001121,50.9577900798939));
#16343=CARTESIAN_POINT('Origin',(-8.88178419700125E-15,25.,36.015352874563));
#16344=CARTESIAN_POINT('',(2.6,25.,28.515352874563));
#16345=CARTESIAN_POINT('',(-1.0547118733939E-14,25.,28.515352874563));
#16346=CARTESIAN_POINT('Origin',(2.6,25.,36.015352874563));
#16347=CARTESIAN_POINT('Origin',(-8.88178419700125E-15,42.6473520600112,
35.4577900798939));
#16348=CARTESIAN_POINT('',(2.6,42.6473520600112,32.9577900798939));
#16349=CARTESIAN_POINT('',(-9.43689570931383E-15,42.6473520600112,32.9577900798939));
#16350=CARTESIAN_POINT('Origin',(2.6,42.6473520600112,35.4577900798939));
#16351=CARTESIAN_POINT('Origin',(-8.88178419700125E-15,30.9806853933445,
19.9577900798938));
#16352=CARTESIAN_POINT('',(2.60000000000001,30.9806853933445,17.4577900798939));
#16353=CARTESIAN_POINT('',(-9.43689570931383E-15,30.9806853933445,17.4577900798939));
#16354=CARTESIAN_POINT('Origin',(2.60000000000001,30.9806853933445,19.9577900798938));
#16355=CARTESIAN_POINT('Origin',(0.,30.9806853933445,50.9577900798939));
#16356=CARTESIAN_POINT('',(2.6,30.9806853933445,48.4577900798939));
#16357=CARTESIAN_POINT('',(-5.55111512312577E-16,30.9806853933445,48.4577900798939));
#16358=CARTESIAN_POINT('Origin',(2.6,30.9806853933445,50.9577900798939));
#16359=CARTESIAN_POINT('Origin',(9.03122179856829,19.3140187266779,59.9890118784622));
#16360=CARTESIAN_POINT('',(11.5312217985683,19.3140187266779,59.9890118784622));
#16361=CARTESIAN_POINT('Origin',(9.03122179856829,19.3140187266779,59.9890118784622));
#16362=CARTESIAN_POINT('',(11.5312217985683,19.3140187266779,57.3890118784622));
#16363=CARTESIAN_POINT('',(11.5312217985683,19.3140187266779,59.9890118784622));
#16364=CARTESIAN_POINT('Origin',(9.03122179856829,19.3140187266779,57.3890118784622));
#16365=CARTESIAN_POINT('Origin',(9.03122179856829,42.6473520600112,59.9890118784622));
#16366=CARTESIAN_POINT('',(11.5312217985683,42.6473520600112,59.9890118784622));
#16367=CARTESIAN_POINT('Origin',(9.03122179856829,42.6473520600112,59.9890118784622));
#16368=CARTESIAN_POINT('',(11.5312217985683,42.6473520600112,57.3890118784622));
#16369=CARTESIAN_POINT('',(11.5312217985683,42.6473520600112,59.9890118784622));
#16370=CARTESIAN_POINT('Origin',(9.03122179856829,42.6473520600112,57.3890118784622));
#16371=CARTESIAN_POINT('Origin',(40.0312217985683,7.64735206001121,59.9890118784622));
#16372=CARTESIAN_POINT('',(42.5312217985683,7.64735206001121,59.9890118784622));
#16373=CARTESIAN_POINT('Origin',(40.0312217985683,7.64735206001121,59.9890118784622));
#16374=CARTESIAN_POINT('',(42.5312217985683,7.64735206001121,57.3890118784622));
#16375=CARTESIAN_POINT('',(42.5312217985683,7.64735206001121,59.9890118784622));
#16376=CARTESIAN_POINT('Origin',(40.0312217985683,7.64735206001121,57.3890118784622));
#16377=CARTESIAN_POINT('Origin',(23.9736590038991,25.,59.9890118784622));
#16378=CARTESIAN_POINT('',(31.4736590038991,25.,59.9890118784622));
#16379=CARTESIAN_POINT('Origin',(23.9736590038991,25.,59.9890118784622));
#16380=CARTESIAN_POINT('',(31.4736590038991,25.,57.3890118784622));
#16381=CARTESIAN_POINT('',(31.4736590038991,25.,59.9890118784622));
#16382=CARTESIAN_POINT('Origin',(23.9736590038991,25.,57.3890118784622));
#16383=CARTESIAN_POINT('Origin',(40.0312217985683,30.9806853933445,59.9890118784622));
#16384=CARTESIAN_POINT('',(42.5312217985683,30.9806853933445,59.9890118784622));
#16385=CARTESIAN_POINT('Origin',(40.0312217985683,30.9806853933445,59.9890118784622));
#16386=CARTESIAN_POINT('',(42.5312217985683,30.9806853933445,57.3890118784622));
#16387=CARTESIAN_POINT('',(42.5312217985683,30.9806853933445,59.9890118784622));
#16388=CARTESIAN_POINT('Origin',(40.0312217985683,30.9806853933445,57.3890118784622));
#16389=CARTESIAN_POINT('Origin',(9.03122179856829,30.9806853933445,59.9890118784622));
#16390=CARTESIAN_POINT('',(11.5312217985683,30.9806853933445,59.9890118784622));
#16391=CARTESIAN_POINT('Origin',(9.03122179856829,30.9806853933445,59.9890118784622));
#16392=CARTESIAN_POINT('',(11.5312217985683,30.9806853933445,57.3890118784622));
#16393=CARTESIAN_POINT('',(11.5312217985683,30.9806853933445,59.9890118784622));
#16394=CARTESIAN_POINT('Origin',(9.03122179856829,30.9806853933445,57.3890118784622));
#16395=CARTESIAN_POINT('Origin',(24.5312217985683,42.6473520600112,59.9890118784622));
#16396=CARTESIAN_POINT('',(27.0312217985683,42.6473520600112,59.9890118784622));
#16397=CARTESIAN_POINT('Origin',(24.5312217985683,42.6473520600112,59.9890118784622));
#16398=CARTESIAN_POINT('',(27.0312217985683,42.6473520600112,57.3890118784622));
#16399=CARTESIAN_POINT('',(27.0312217985683,42.6473520600112,59.9890118784622));
#16400=CARTESIAN_POINT('Origin',(24.5312217985683,42.6473520600112,57.3890118784622));
#16401=CARTESIAN_POINT('Origin',(9.03122179856829,7.64735206001121,59.9890118784622));
#16402=CARTESIAN_POINT('',(11.5312217985683,7.64735206001121,59.9890118784622));
#16403=CARTESIAN_POINT('Origin',(9.03122179856829,7.64735206001121,59.9890118784622));
#16404=CARTESIAN_POINT('',(11.5312217985683,7.64735206001121,57.3890118784622));
#16405=CARTESIAN_POINT('',(11.5312217985683,7.64735206001121,59.9890118784622));
#16406=CARTESIAN_POINT('Origin',(9.03122179856829,7.64735206001121,57.3890118784622));
#16407=CARTESIAN_POINT('Origin',(24.5312217985683,7.64735206001121,59.9890118784622));
#16408=CARTESIAN_POINT('',(27.0312217985683,7.64735206001121,59.9890118784622));
#16409=CARTESIAN_POINT('Origin',(24.5312217985683,7.64735206001121,59.9890118784622));
#16410=CARTESIAN_POINT('',(27.0312217985683,7.64735206001121,57.3890118784622));
#16411=CARTESIAN_POINT('',(27.0312217985683,7.64735206001121,59.9890118784622));
#16412=CARTESIAN_POINT('Origin',(24.5312217985683,7.64735206001121,57.3890118784622));
#16413=CARTESIAN_POINT('Origin',(40.0312217985683,42.6473520600112,59.9890118784622));
#16414=CARTESIAN_POINT('',(42.5312217985683,42.6473520600112,59.9890118784622));
#16415=CARTESIAN_POINT('Origin',(40.0312217985683,42.6473520600112,59.9890118784622));
#16416=CARTESIAN_POINT('',(42.5312217985683,42.6473520600112,57.3890118784622));
#16417=CARTESIAN_POINT('',(42.5312217985683,42.6473520600112,59.9890118784622));
#16418=CARTESIAN_POINT('Origin',(40.0312217985683,42.6473520600112,57.3890118784622));
#16419=CARTESIAN_POINT('Origin',(40.0312217985683,19.3140187266779,59.9890118784622));
#16420=CARTESIAN_POINT('',(42.5312217985683,19.3140187266779,59.9890118784622));
#16421=CARTESIAN_POINT('Origin',(40.0312217985683,19.3140187266779,59.9890118784622));
#16422=CARTESIAN_POINT('',(42.5312217985683,19.3140187266779,57.3890118784622));
#16423=CARTESIAN_POINT('',(42.5312217985683,19.3140187266779,59.9890118784622));
#16424=CARTESIAN_POINT('Origin',(40.0312217985683,19.3140187266779,57.3890118784622));
#16425=CARTESIAN_POINT('Origin',(47.9473180077982,0.,59.9890118784622));
#16426=CARTESIAN_POINT('',(47.9473180077982,50.,57.3890118784622));
#16427=CARTESIAN_POINT('',(47.9473180077982,0.,57.3890118784622));
#16428=CARTESIAN_POINT('',(47.9473180077982,50.,59.9890118784622));
#16429=CARTESIAN_POINT('',(47.9473180077982,50.,12.));
#16430=CARTESIAN_POINT('',(47.9473180077982,0.,59.9890118784622));
#16431=CARTESIAN_POINT('Origin',(0.,0.,59.9890118784622));
#16432=CARTESIAN_POINT('',(47.9473180077982,50.,59.9890118784622));
#16433=CARTESIAN_POINT('Origin',(47.9473180077982,0.,12.));
#16434=CARTESIAN_POINT('',(47.9473180077982,50.,12.));
#16435=CARTESIAN_POINT('',(0.,50.,12.));
#16436=CARTESIAN_POINT('',(47.9473180077982,0.,12.));
#16437=CARTESIAN_POINT('Origin',(47.9473180077982,0.,14.6));
#16438=CARTESIAN_POINT('',(47.9473180077982,50.,14.6));
#16439=CARTESIAN_POINT('',(47.9473180077982,50.,12.));
#16440=CARTESIAN_POINT('',(47.9473180077982,0.,14.6));
#16441=CARTESIAN_POINT('Origin',(2.6,0.,14.6));
#16442=CARTESIAN_POINT('',(2.6,50.,14.6));
#16443=CARTESIAN_POINT('',(2.6,50.,14.6));
#16444=CARTESIAN_POINT('',(2.6,0.,14.6));
#16445=CARTESIAN_POINT('Origin',(2.6,0.,57.3890118784622));
#16446=CARTESIAN_POINT('',(2.6,50.,57.3890118784622));
#16447=CARTESIAN_POINT('',(2.6,50.,57.3890118784622));
#16448=CARTESIAN_POINT('',(2.6,0.,57.3890118784622));
#16449=CARTESIAN_POINT('Origin',(47.9473180077982,0.,57.3890118784622));
#16450=CARTESIAN_POINT('',(47.9473180077982,50.,57.3890118784622));
#16451=CARTESIAN_POINT('Origin',(23.9736590038991,50.,35.9945059392311));
#19192=UNCERTAINTY_MEASURE_WITH_UNIT(LENGTH_MEASURE(0.01),#19221,
'DISTANCE_ACCURACY_VALUE',
'Maximum model space distance between geometric entities at asserted c
onnectivities');
#19204=UNCERTAINTY_MEASURE_WITH_UNIT(LENGTH_MEASURE(0.01),#19221,
'DISTANCE_ACCURACY_VALUE',
'Maximum model space distance between geometric entities at asserted c
onnectivities');
#19208=(
GEOMETRIC_REPRESENTATION_CONTEXT(3)
GLOBAL_UNCERTAINTY_ASSIGNED_CONTEXT((#19192))
GLOBAL_UNIT_ASSIGNED_CONTEXT((#19221,#19223,#19224))
REPRESENTATION_CONTEXT('','3D')
);
#19220=(
GEOMETRIC_REPRESENTATION_CONTEXT(3)
GLOBAL_UNCERTAINTY_ASSIGNED_CONTEXT((#19204))
GLOBAL_UNIT_ASSIGNED_CONTEXT((#19221,#19223,#19224))
REPRESENTATION_CONTEXT('','3D')
);
#19221=(
LENGTH_UNIT()
NAMED_UNIT(*)
SI_UNIT(.MILLI.,.METRE.)
);
#19223=(
NAMED_UNIT(*)
PLANE_ANGLE_UNIT()
SI_UNIT($,.RADIAN.)
);
#19224=(
NAMED_UNIT(*)
SI_UNIT($,.STERADIAN.)
SOLID_ANGLE_UNIT()
);
#19228=SHAPE_DEFINITION_REPRESENTATION(#19243,#19272);
#19243=PRODUCT_DEFINITION_SHAPE('',$,#19288);
#19272=SHAPE_REPRESENTATION('',(#11555),#19208);
#19284=PRODUCT_DEFINITION_CONTEXT('part definition',#19331,'design');
#19288=PRODUCT_DEFINITION('Motor_Mount (1)','Motor_Mount (1)',#19303,#19284);
#19303=PRODUCT_DEFINITION_FORMATION('',$,#19336);
#19331=APPLICATION_CONTEXT(
'Core Data for Automotive Mechanical Design Process');
#19332=PRODUCT_CONTEXT('part definition',#19331,'mechanical');
#19336=PRODUCT('Motor_Mount (1)','Motor_Mount (1)',$,(#19332));
#19411=COLOUR_RGB('Off White',0.89,0.88,0.83);
#19412=FILL_AREA_STYLE_COLOUR('',#19411);
#19413=FILL_AREA_STYLE('',(#19412));
#19414=SURFACE_STYLE_FILL_AREA(#19413);
#19415=SURFACE_SIDE_STYLE('',(#19414));
#19416=SURFACE_STYLE_USAGE(.BOTH.,#19415);
#19417=PRESENTATION_STYLE_ASSIGNMENT((#19416));
ENDSEC;
END-ISO-10303-21;
